ISO-10303-21;
HEADER;
/* Generated by software containing ST-Developer
 * from STEP Tools, Inc. (www.steptools.com) 
 */

FILE_DESCRIPTION(
/* description */ (''),
/* implementation_level */ '2;1');

FILE_NAME(
/* name */ 'Nut.step',
/* time_stamp */ '2026-10-07T02:13:48+06:00',
/* author */ (''),
/* organization */ (''),
/* preprocessor_version */ 'ST-DEVELOPER v20.2',
/* originating_system */ 'Autodesk Translation Framework v15.15.0.0',
/* authorisation */ '');

FILE_SCHEMA (('AUTOMOTIVE_DESIGN { 1 0 10303 214 3 1 1 }'));
ENDSEC;

DATA;
#10=MECHANICAL_DESIGN_GEOMETRIC_PRESENTATION_REPRESENTATION('',(#120),#17042);
#84=B_SPLINE_SURFACE_WITH_KNOTS('',3,3,((#14832,#14833,#14834,#14835,#14836,
#14837,#14838,#14839,#14840,#14841,#14842,#14843,#14844,#14845,#14846,#14847,
#14848,#14849,#14850,#14851,#14852,#14853,#14854,#14855,#14856,#14857,#14858,
#14859,#14860,#14861,#14862,#14863,#14864,#14865,#14866,#14867,#14868,#14869,
#14870,#14871,#14872,#14873,#14874,#14875,#14876,#14877,#14878,#14879,#14880,
#14881,#14882,#14883,#14884,#14885,#14886,#14887,#14888,#14889,#14890,#14891,
#14892,#14893,#14894,#14895,#14896,#14897,#14898,#14899,#14900,#14901,#14902,
#14903,#14904,#14905,#14906,#14907,#14908,#14909,#14910),(#14911,#14912,
#14913,#14914,#14915,#14916,#14917,#14918,#14919,#14920,#14921,#14922,#14923,
#14924,#14925,#14926,#14927,#14928,#14929,#14930,#14931,#14932,#14933,#14934,
#14935,#14936,#14937,#14938,#14939,#14940,#14941,#14942,#14943,#14944,#14945,
#14946,#14947,#14948,#14949,#14950,#14951,#14952,#14953,#14954,#14955,#14956,
#14957,#14958,#14959,#14960,#14961,#14962,#14963,#14964,#14965,#14966,#14967,
#14968,#14969,#14970,#14971,#14972,#14973,#14974,#14975,#14976,#14977,#14978,
#14979,#14980,#14981,#14982,#14983,#14984,#14985,#14986,#14987,#14988,#14989),
(#14990,#14991,#14992,#14993,#14994,#14995,#14996,#14997,#14998,#14999,
#15000,#15001,#15002,#15003,#15004,#15005,#15006,#15007,#15008,#15009,#15010,
#15011,#15012,#15013,#15014,#15015,#15016,#15017,#15018,#15019,#15020,#15021,
#15022,#15023,#15024,#15025,#15026,#15027,#15028,#15029,#15030,#15031,#15032,
#15033,#15034,#15035,#15036,#15037,#15038,#15039,#15040,#15041,#15042,#15043,
#15044,#15045,#15046,#15047,#15048,#15049,#15050,#15051,#15052,#15053,#15054,
#15055,#15056,#15057,#15058,#15059,#15060,#15061,#15062,#15063,#15064,#15065,
#15066,#15067,#15068),(#15069,#15070,#15071,#15072,#15073,#15074,#15075,
#15076,#15077,#15078,#15079,#15080,#15081,#15082,#15083,#15084,#15085,#15086,
#15087,#15088,#15089,#15090,#15091,#15092,#15093,#15094,#15095,#15096,#15097,
#15098,#15099,#15100,#15101,#15102,#15103,#15104,#15105,#15106,#15107,#15108,
#15109,#15110,#15111,#15112,#15113,#15114,#15115,#15116,#15117,#15118,#15119,
#15120,#15121,#15122,#15123,#15124,#15125,#15126,#15127,#15128,#15129,#15130,
#15131,#15132,#15133,#15134,#15135,#15136,#15137,#15138,#15139,#15140,#15141,
#15142,#15143,#15144,#15145,#15146,#15147)),.UNSPECIFIED.,.F.,.F.,.F.,(4,
4),(4,1,1,1,1,1,1,1,1,1,1,1,1,1,1,1,1,1,1,1,1,1,1,1,1,1,1,1,1,1,1,1,1,1,
1,1,1,1,1,1,1,1,1,1,1,1,1,1,1,1,1,1,1,1,1,1,1,1,1,1,1,1,1,1,1,1,1,1,1,1,
1,1,1,1,1,1,4),(0.,0.0820126057383859),(8.31487785380719,8.80497047640879,
9.29506309901039,9.78515572161199,10.2752483442136,10.7653409668152,11.2554335894168,
11.7455262120184,12.23561883462,12.7257114572216,13.2158040798232,13.7058967024248,
14.1959893250264,14.686081947628,15.1761745702296,15.6662671928312,16.1563598154328,
16.6464524380344,17.136545060636,17.6266376832376,18.1167303058392,18.6068229284408,
19.0969155510424,19.587008173644,20.0771007962456,20.5671934188472,21.0572860414487,
21.5473786640503,22.0374712866519,22.5275639092535,23.0176565318551,23.5077491544567,
23.9978417770583,24.4879343996599,24.9780270222615,25.4681196448631,25.9582122674647,
26.4483048900663,26.9383975126679,27.4284901352695,27.9185827578711,28.4086753804727,
28.8987680030743,29.3888606256759,29.8789532482775,30.3690458708791,30.8591384934807,
31.3492311160823,31.8393237386839,32.3294163612855,32.8195089838871,33.3096016064887,
33.7996942290903,34.2897868516919,34.7798794742935,35.2699720968951,35.7600647194967,
36.2501573420983,36.7402499646999,37.2303425873015,37.7204352099031,38.2105278325047,
38.7006204551063,39.1907130777079,39.6808057003095,40.1708983229111,40.6609909455127,
41.1510835681143,41.6411761907159,42.1312688133175,42.6213614359191,43.1114540585207,
43.6015466811223,44.0916393037239,44.5817319263255,45.0718245489271,45.5619171715287),
 .UNSPECIFIED.);
#85=B_SPLINE_SURFACE_WITH_KNOTS('',3,3,((#15435,#15436,#15437,#15438,#15439,
#15440,#15441,#15442,#15443,#15444,#15445,#15446,#15447,#15448,#15449,#15450,
#15451,#15452,#15453,#15454,#15455,#15456,#15457,#15458,#15459,#15460,#15461,
#15462,#15463,#15464,#15465,#15466,#15467,#15468,#15469,#15470,#15471,#15472,
#15473,#15474,#15475,#15476,#15477,#15478,#15479,#15480,#15481,#15482,#15483,
#15484,#15485,#15486,#15487,#15488,#15489,#15490,#15491,#15492,#15493,#15494,
#15495,#15496,#15497,#15498,#15499,#15500,#15501,#15502,#15503,#15504,#15505,
#15506,#15507,#15508,#15509,#15510,#15511,#15512,#15513),(#15514,#15515,
#15516,#15517,#15518,#15519,#15520,#15521,#15522,#15523,#15524,#15525,#15526,
#15527,#15528,#15529,#15530,#15531,#15532,#15533,#15534,#15535,#15536,#15537,
#15538,#15539,#15540,#15541,#15542,#15543,#15544,#15545,#15546,#15547,#15548,
#15549,#15550,#15551,#15552,#15553,#15554,#15555,#15556,#15557,#15558,#15559,
#15560,#15561,#15562,#15563,#15564,#15565,#15566,#15567,#15568,#15569,#15570,
#15571,#15572,#15573,#15574,#15575,#15576,#15577,#15578,#15579,#15580,#15581,
#15582,#15583,#15584,#15585,#15586,#15587,#15588,#15589,#15590,#15591,#15592),
(#15593,#15594,#15595,#15596,#15597,#15598,#15599,#15600,#15601,#15602,
#15603,#15604,#15605,#15606,#15607,#15608,#15609,#15610,#15611,#15612,#15613,
#15614,#15615,#15616,#15617,#15618,#15619,#15620,#15621,#15622,#15623,#15624,
#15625,#15626,#15627,#15628,#15629,#15630,#15631,#15632,#15633,#15634,#15635,
#15636,#15637,#15638,#15639,#15640,#15641,#15642,#15643,#15644,#15645,#15646,
#15647,#15648,#15649,#15650,#15651,#15652,#15653,#15654,#15655,#15656,#15657,
#15658,#15659,#15660,#15661,#15662,#15663,#15664,#15665,#15666,#15667,#15668,
#15669,#15670,#15671),(#15672,#15673,#15674,#15675,#15676,#15677,#15678,
#15679,#15680,#15681,#15682,#15683,#15684,#15685,#15686,#15687,#15688,#15689,
#15690,#15691,#15692,#15693,#15694,#15695,#15696,#15697,#15698,#15699,#15700,
#15701,#15702,#15703,#15704,#15705,#15706,#15707,#15708,#15709,#15710,#15711,
#15712,#15713,#15714,#15715,#15716,#15717,#15718,#15719,#15720,#15721,#15722,
#15723,#15724,#15725,#15726,#15727,#15728,#15729,#15730,#15731,#15732,#15733,
#15734,#15735,#15736,#15737,#15738,#15739,#15740,#15741,#15742,#15743,#15744,
#15745,#15746,#15747,#15748,#15749,#15750)),.UNSPECIFIED.,.F.,.F.,.F.,(4,
4),(4,1,1,1,1,1,1,1,1,1,1,1,1,1,1,1,1,1,1,1,1,1,1,1,1,1,1,1,1,1,1,1,1,1,
1,1,1,1,1,1,1,1,1,1,1,1,1,1,1,1,1,1,1,1,1,1,1,1,1,1,1,1,1,1,1,1,1,1,1,1,
1,1,1,1,1,1,4),(0.,0.0820126057383859),(11.6150691238056,12.1051617464072,
12.5952543690088,13.0853469916104,13.575439614212,14.0655322368136,14.5556248594152,
15.0457174820168,15.5358101046184,16.02590272722,16.5159953498216,17.0060879724232,
17.4961805950248,17.9862732176264,18.476365840228,18.9664584628296,19.4565510854312,
19.9466437080328,20.4367363306344,20.926828953236,21.4169215758376,21.9070141984391,
22.3971068210408,22.8871994436423,23.3772920662439,23.8673846888455,24.3574773114471,
24.8475699340487,25.3376625566503,25.8277551792519,26.3178478018535,26.8079404244551,
27.2980330470567,27.7881256696583,28.2782182922599,28.7683109148615,29.2584035374631,
29.7484961600647,30.2385887826663,30.7286814052679,31.2187740278695,31.7088666504711,
32.1989592730727,32.6890518956743,33.1791445182759,33.6692371408775,34.1593297634791,
34.6494223860807,35.1395150086823,35.6296076312839,36.1197002538855,36.6097928764871,
37.0998854990887,37.5899781216903,38.0800707442919,38.5701633668935,39.0602559894951,
39.5503486120967,40.0404412346983,40.5305338572999,41.0206264799015,41.5107191025031,
42.0008117251047,42.4909043477063,42.9809969703079,43.4710895929095,43.9611822155111,
44.4512748381127,44.9413674607143,45.4314600833159,45.9215527059175,46.4116453285191,
46.9017379511207,47.3918305737223,47.8819231963239,48.3720158189255,48.8621084415271),
 .UNSPECIFIED.);
#96=SHAPE_REPRESENTATION_RELATIONSHIP('SRR','None',#17092,#108);
#108=ADVANCED_BREP_SHAPE_REPRESENTATION('',(#132),#17036);
#120=STYLED_ITEM('',(#17154),#132);
#132=MANIFOLD_SOLID_BREP('Body1',#8121);
#168=FACE_BOUND('',#1324,.T.);
#169=FACE_BOUND('',#1327,.T.);
#170=FACE_BOUND('',#1329,.T.);
#402=PLANE('',#8924);
#403=PLANE('',#8929);
#404=PLANE('',#8931);
#802=FACE_OUTER_BOUND('',#1309,.T.);
#803=FACE_OUTER_BOUND('',#1310,.T.);
#804=FACE_OUTER_BOUND('',#1311,.T.);
#805=FACE_OUTER_BOUND('',#1312,.T.);
#806=FACE_OUTER_BOUND('',#1313,.T.);
#807=FACE_OUTER_BOUND('',#1314,.T.);
#808=FACE_OUTER_BOUND('',#1315,.T.);
#809=FACE_OUTER_BOUND('',#1316,.T.);
#810=FACE_OUTER_BOUND('',#1317,.T.);
#811=FACE_OUTER_BOUND('',#1318,.T.);
#812=FACE_OUTER_BOUND('',#1319,.T.);
#813=FACE_OUTER_BOUND('',#1320,.T.);
#814=FACE_OUTER_BOUND('',#1321,.T.);
#815=FACE_OUTER_BOUND('',#1322,.T.);
#816=FACE_OUTER_BOUND('',#1323,.T.);
#817=FACE_OUTER_BOUND('',#1325,.T.);
#818=FACE_OUTER_BOUND('',#1326,.T.);
#819=FACE_OUTER_BOUND('',#1328,.T.);
#820=FACE_OUTER_BOUND('',#1330,.T.);
#821=FACE_OUTER_BOUND('',#1331,.T.);
#1309=EDGE_LOOP('',(#6693,#6694,#6695,#6696));
#1310=EDGE_LOOP('',(#6697,#6698,#6699,#6700));
#1311=EDGE_LOOP('',(#6701,#6702,#6703,#6704));
#1312=EDGE_LOOP('',(#6705,#6706,#6707,#6708));
#1313=EDGE_LOOP('',(#6709,#6710,#6711,#6712));
#1314=EDGE_LOOP('',(#6713,#6714,#6715,#6716));
#1315=EDGE_LOOP('',(#6717,#6718,#6719,#6720));
#1316=EDGE_LOOP('',(#6721,#6722,#6723,#6724));
#1317=EDGE_LOOP('',(#6725,#6726,#6727,#6728));
#1318=EDGE_LOOP('',(#6729,#6730,#6731,#6732));
#1319=EDGE_LOOP('',(#6733,#6734,#6735,#6736));
#1320=EDGE_LOOP('',(#6737,#6738,#6739,#6740,#6741,#6742,#6743,#6744,#6745,
#6746,#6747,#6748,#6749,#6750,#6751));
#1321=EDGE_LOOP('',(#6752,#6753,#6754,#6755));
#1322=EDGE_LOOP('',(#6756,#6757,#6758,#6759,#6760,#6761,#6762,#6763,#6764,
#6765,#6766,#6767,#6768,#6769,#6770));
#1323=EDGE_LOOP('',(#6771));
#1324=EDGE_LOOP('',(#6772,#6773,#6774,#6775));
#1325=EDGE_LOOP('',(#6776,#6777,#6778,#6779));
#1326=EDGE_LOOP('',(#6780));
#1327=EDGE_LOOP('',(#6781));
#1328=EDGE_LOOP('',(#6782,#6783,#6784,#6785));
#1329=EDGE_LOOP('',(#6786));
#1330=EDGE_LOOP('',(#6787,#6788,#6789,#6790));
#1331=EDGE_LOOP('',(#6791,#6792,#6793,#6794));
#1810=CIRCLE('',#8910,8.866);
#1811=CIRCLE('',#8917,7.4455);
#1812=CIRCLE('',#8923,7.4455);
#1813=CIRCLE('',#8925,11.);
#1814=CIRCLE('',#8926,8.866);
#1815=CIRCLE('',#8928,11.);
#1816=CIRCLE('',#8930,7.);
#1817=CIRCLE('',#8932,7.);
#1976=B_SPLINE_CURVE_WITH_KNOTS('',3,(#14174,#14175,#14176,#14177,#14178,
#14179,#14180,#14181,#14182,#14183,#14184,#14185,#14186,#14187,#14188,#14189),
 .UNSPECIFIED.,.F.,.F.,(4,3,3,3,3,4),(-4.09289414414334,-3.92074098081279,
-3.43064835821119,-2.94055573560959,-2.45046311300799,-2.06120159751572),
 .UNSPECIFIED.);
#1977=B_SPLINE_CURVE_WITH_KNOTS('',3,(#14192,#14193,#14194,#14195,#14196,
#14197,#14198,#14199,#14200,#14201),.UNSPECIFIED.,.F.,.F.,(4,3,3,4),(0.,
0.490092622601601,0.980185245203199,1.10990010696217),.UNSPECIFIED.);
#1978=B_SPLINE_CURVE_WITH_KNOTS('',3,(#14206,#14207,#14208,#14209,#14210,
#14211,#14212,#14213,#14214,#14215,#14216,#14217,#14218,#14219,#14220,#14221,
#14222,#14223,#14224,#14225,#14226,#14227,#14228,#14229,#14230,#14231,#14232,
#14233,#14234,#14235,#14236,#14237,#14238,#14239,#14240,#14241,#14242,#14243,
#14244,#14245,#14246,#14247,#14248),.UNSPECIFIED.,.F.,.F.,(4,3,3,3,3,3,
3,3,3,3,3,3,3,3,4),(-10.3760794513229,-10.2919450746336,-9.80185245203197,
-9.31175982943038,-8.82166720682877,-8.33157458422717,-7.84148196162558,
-7.35138933902398,-6.86129671642238,-6.37120409382078,-5.88111147121918,
-5.39101884861759,-4.90092622601599,-4.41083360341439,-4.09289414414334),
 .UNSPECIFIED.);
#1979=B_SPLINE_CURVE_WITH_KNOTS('',3,(#14249,#14250,#14251,#14252,#14253,
#14254,#14255,#14256,#14257,#14258,#14259,#14260,#14261,#14262,#14263,#14264,
#14265,#14266,#14267,#14268,#14269,#14270,#14271,#14272,#14273,#14274,#14275,
#14276,#14277,#14278,#14279,#14280,#14281,#14282,#14283,#14284,#14285,#14286,
#14287,#14288,#14289,#14290,#14291),.UNSPECIFIED.,.F.,.F.,(4,3,3,3,3,3,
3,3,3,3,3,3,3,3,4),(1.10990010696217,1.4702778678048,1.9603704904064,2.450463113008,
2.94055573560959,3.43064835821119,3.92074098081279,4.41083360341439,4.90092622601598,
5.39101884861758,5.88111147121918,6.37120409382078,6.86129671642238,7.35138933902397,
7.39308541414175),.UNSPECIFIED.);
#1980=B_SPLINE_CURVE_WITH_KNOTS('',3,(#14296,#14297,#14298,#14299,#14300,
#14301,#14302,#14303,#14304,#14305,#14306,#14307,#14308,#14309,#14310,#14311,
#14312,#14313,#14314,#14315,#14316,#14317,#14318,#14319,#14320,#14321,#14322,
#14323,#14324,#14325,#14326,#14327,#14328,#14329,#14330,#14331,#14332,#14333,
#14334,#14335),.UNSPECIFIED.,.F.,.F.,(4,3,3,3,3,3,3,3,3,3,3,3,3,4),(-16.6592647585025,
-16.1730565458528,-15.6829639232512,-15.1928713006496,-14.702778678048,
-14.2126860554464,-13.7225934328448,-13.2325008102432,-12.7424081876416,
-12.25231556504,-11.7622229424384,-11.2721303198368,-10.7820376972352,-10.3760794513229),
 .UNSPECIFIED.);
#1981=B_SPLINE_CURVE_WITH_KNOTS('',3,(#14336,#14337,#14338,#14339,#14340,
#14341,#14342,#14343,#14344,#14345,#14346,#14347,#14348,#14349,#14350,#14351,
#14352,#14353,#14354,#14355,#14356,#14357,#14358,#14359,#14360,#14361,#14362,
#14363,#14364,#14365,#14366,#14367,#14368,#14369,#14370,#14371,#14372,#14373,
#14374,#14375),.UNSPECIFIED.,.F.,.F.,(4,3,3,3,3,3,3,3,3,3,3,3,3,4),(7.39308541414175,
7.84148196162557,8.33157458422717,8.82166720682877,9.31175982943037,9.80185245203197,
10.2919450746336,10.7820376972352,11.2721303198368,11.7622229424384,12.25231556504,
12.7424081876416,13.2325008102432,13.6762707213213),.UNSPECIFIED.);
#1982=B_SPLINE_CURVE_WITH_KNOTS('',3,(#14380,#14381,#14382,#14383,#14384,
#14385,#14386,#14387,#14388,#14389,#14390,#14391,#14392,#14393,#14394,#14395,
#14396,#14397,#14398,#14399,#14400,#14401,#14402,#14403,#14404,#14405,#14406,
#14407,#14408,#14409,#14410,#14411,#14412,#14413,#14414,#14415,#14416,#14417,
#14418,#14419,#14420,#14421,#14422),.UNSPECIFIED.,.F.,.F.,(4,3,3,3,3,3,
3,3,3,3,3,3,3,3,4),(-22.9424500656821,-22.5442606396735,-22.0541680170719,
-21.5640753944703,-21.0739827718687,-20.5838901492671,-20.0937975266655,
-19.6037049040639,-19.1136122814623,-18.6235196588607,-18.1334270362591,
-17.6433344136575,-17.153241791056,-16.6631491684543,-16.6592647585025),
 .UNSPECIFIED.);
#1983=B_SPLINE_CURVE_WITH_KNOTS('',3,(#14423,#14424,#14425,#14426,#14427,
#14428,#14429,#14430,#14431,#14432,#14433,#14434,#14435,#14436,#14437,#14438,
#14439,#14440,#14441,#14442,#14443,#14444,#14445,#14446,#14447,#14448,#14449,
#14450,#14451,#14452,#14453,#14454,#14455,#14456,#14457,#14458,#14459,#14460,
#14461,#14462,#14463,#14464,#14465),.UNSPECIFIED.,.F.,.F.,(4,3,3,3,3,3,
3,3,3,3,3,3,3,3,4),(13.6762707213213,13.7225934328448,14.2126860554464,
14.702778678048,15.1928713006496,15.6829639232512,16.1730565458528,16.6631491684543,
17.1532417910559,17.6433344136575,18.1334270362591,18.6235196588607,19.1136122814623,
19.6037049040639,19.9594560285009),.UNSPECIFIED.);
#1984=B_SPLINE_CURVE_WITH_KNOTS('',3,(#14470,#14471,#14472,#14473,#14474,
#14475,#14476,#14477,#14478,#14479,#14480,#14481,#14482,#14483,#14484,#14485,
#14486,#14487,#14488,#14489,#14490,#14491,#14492,#14493,#14494,#14495,#14496,
#14497,#14498,#14499,#14500,#14501,#14502,#14503,#14504,#14505,#14506,#14507,
#14508,#14509,#14510,#14511,#14512),.UNSPECIFIED.,.F.,.F.,(4,3,3,3,3,3,
3,3,3,3,3,3,3,3,4),(-29.2256353728617,-28.9154647334943,-28.4253721108927,
-27.9352794882911,-27.4451868656895,-26.9550942430879,-26.4650016204863,
-25.9749089978847,-25.4848163752831,-24.9947237526815,-24.5046311300799,
-24.0145385074783,-23.5244458848767,-23.0343532622751,-22.9424500656821),
 .UNSPECIFIED.);
#1985=B_SPLINE_CURVE_WITH_KNOTS('',3,(#14513,#14514,#14515,#14516,#14517,
#14518,#14519,#14520,#14521,#14522,#14523,#14524,#14525,#14526,#14527,#14528,
#14529,#14530,#14531,#14532,#14533,#14534,#14535,#14536,#14537,#14538,#14539,
#14540,#14541,#14542,#14543,#14544,#14545,#14546,#14547,#14548,#14549,#14550,
#14551,#14552,#14553,#14554,#14555),.UNSPECIFIED.,.F.,.F.,(4,3,3,3,3,3,
3,3,3,3,3,3,3,3,4),(19.9594560285009,20.0937975266655,20.5838901492671,
21.0739827718687,21.5640753944703,22.0541680170719,22.5442606396735,23.0343532622751,
23.5244458848767,24.0145385074783,24.5046311300799,24.9947237526815,25.4848163752831,
25.9749089978847,26.2426413356805),.UNSPECIFIED.);
#1986=B_SPLINE_CURVE_WITH_KNOTS('',3,(#14560,#14561,#14562,#14563,#14564,
#14565,#14566,#14567,#14568,#14569,#14570,#14571,#14572,#14573,#14574,#14575,
#14576,#14577,#14578,#14579,#14580,#14581,#14582,#14583,#14584,#14585,#14586,
#14587,#14588,#14589,#14590,#14591,#14592,#14593,#14594,#14595,#14596,#14597,
#14598,#14599,#14600,#14601,#14602),.UNSPECIFIED.,.F.,.F.,(4,3,3,3,3,3,
3,3,3,3,3,3,3,3,4),(-35.5088206800413,-35.2866688273151,-34.7965762047135,
-34.3064835821119,-33.8163909595103,-33.3262983369087,-32.8362057143071,
-32.3461130917055,-31.8560204691039,-31.3659278465023,-30.8758352239007,
-30.3857426012991,-29.8956499786975,-29.4055573560959,-29.2256353728617),
 .UNSPECIFIED.);
#1987=B_SPLINE_CURVE_WITH_KNOTS('',3,(#14603,#14604,#14605,#14606,#14607,
#14608,#14609,#14610,#14611,#14612,#14613,#14614,#14615,#14616,#14617,#14618,
#14619,#14620,#14621,#14622,#14623,#14624,#14625,#14626,#14627,#14628,#14629,
#14630,#14631,#14632,#14633,#14634,#14635,#14636,#14637,#14638,#14639,#14640,
#14641,#14642,#14643,#14644,#14645),.UNSPECIFIED.,.F.,.F.,(4,3,3,3,3,3,
3,3,3,3,3,3,3,3,4),(26.2426413356805,26.4650016204863,26.9550942430879,
27.4451868656895,27.9352794882911,28.4253721108927,28.9154647334943,29.4055573560959,
29.8956499786975,30.3857426012991,30.8758352239007,31.3659278465023,31.8560204691039,
32.3461130917055,32.5258266428601),.UNSPECIFIED.);
#1988=B_SPLINE_CURVE_WITH_KNOTS('',3,(#14651,#14652,#14653,#14654,#14655,
#14656,#14657,#14658,#14659,#14660,#14661,#14662,#14663,#14664,#14665,#14666),
 .UNSPECIFIED.,.F.,.F.,(4,1,1,1,1,1,1,1,1,1,1,1,1,4),(40.8407044966673,
41.0206264799015,41.5107191025031,42.0008117251047,42.4909043477063,42.9809969703079,
43.4710895929095,43.9611822155111,44.4512748381127,44.9413674607143,45.4314600833159,
45.9215527059175,46.4116453285191,46.8009068440113),.UNSPECIFIED.);
#1989=B_SPLINE_CURVE_WITH_KNOTS('',3,(#14669,#14670,#14671,#14672,#14673,
#14674,#14675,#14676,#14677,#14678,#14679,#14680,#14681),.UNSPECIFIED.,
 .F.,.F.,(4,1,1,1,1,1,1,1,1,1,4),(40.8407044966673,41.1510835681143,41.6411761907159,
42.1312688133175,42.6213614359191,43.1114540585207,43.6015466811223,44.0916393037239,
44.5817319263255,45.0718245489271,45.5619171715287),.UNSPECIFIED.);
#1990=B_SPLINE_CURVE_WITH_KNOTS('',3,(#14686,#14687,#14688,#14689,#14690,
#14691,#14692,#14693,#14694,#14695,#14696,#14697,#14698,#14699,#14700,#14701,
#14702),.UNSPECIFIED.,.F.,.F.,(4,1,1,1,1,1,1,1,1,1,1,1,1,1,4),(34.5575191894877,
34.6494223860807,35.1395150086823,35.6296076312839,36.1197002538855,36.6097928764871,
37.0998854990887,37.5899781216903,38.0800707442919,38.5701633668935,39.0602559894951,
39.5503486120967,40.0404412346983,40.5305338572999,40.8407044966673),
 .UNSPECIFIED.);
#1991=B_SPLINE_CURVE_WITH_KNOTS('',3,(#14703,#14704,#14705,#14706,#14707,
#14708,#14709,#14710,#14711,#14712,#14713,#14714,#14715,#14716,#14717,#14718,
#14719),.UNSPECIFIED.,.F.,.F.,(4,1,1,1,1,1,1,1,1,1,1,1,1,1,4),(34.5575191894877,
34.7798794742935,35.2699720968951,35.7600647194967,36.2501573420983,36.7402499646999,
37.2303425873015,37.7204352099031,38.2105278325047,38.7006204551063,39.1907130777079,
39.6808057003095,40.1708983229111,40.6609909455127,40.8407044966673),
 .UNSPECIFIED.);
#1992=B_SPLINE_CURVE_WITH_KNOTS('',3,(#14724,#14725,#14726,#14727,#14728,
#14729,#14730,#14731,#14732,#14733,#14734,#14735,#14736,#14737,#14738,#14739,
#14740),.UNSPECIFIED.,.F.,.F.,(4,1,1,1,1,1,1,1,1,1,1,1,1,1,4),(28.2743338823081,
28.2782182922599,28.7683109148615,29.2584035374631,29.7484961600647,30.2385887826663,
30.7286814052679,31.2187740278695,31.7088666504711,32.1989592730727,32.6890518956743,
33.1791445182759,33.6692371408775,34.1593297634791,34.5575191894877),
 .UNSPECIFIED.);
#1993=B_SPLINE_CURVE_WITH_KNOTS('',3,(#14741,#14742,#14743,#14744,#14745,
#14746,#14747,#14748,#14749,#14750,#14751,#14752,#14753,#14754,#14755,#14756,
#14757),.UNSPECIFIED.,.F.,.F.,(4,1,1,1,1,1,1,1,1,1,1,1,1,1,4),(28.2743338823081,
28.4086753804727,28.8987680030743,29.3888606256759,29.8789532482775,30.3690458708791,
30.8591384934807,31.3492311160823,31.8393237386839,32.3294163612855,32.8195089838871,
33.3096016064887,33.7996942290903,34.2897868516919,34.5575191894877),
 .UNSPECIFIED.);
#1994=B_SPLINE_CURVE_WITH_KNOTS('',3,(#14762,#14763,#14764,#14765,#14766,
#14767,#14768,#14769,#14770,#14771,#14772,#14773,#14774,#14775,#14776,#14777),
 .UNSPECIFIED.,.F.,.F.,(4,1,1,1,1,1,1,1,1,1,1,1,1,4),(21.9911485751285,
22.3971068210408,22.8871994436423,23.3772920662439,23.8673846888455,24.3574773114471,
24.8475699340487,25.3376625566503,25.8277551792519,26.3178478018535,26.8079404244551,
27.2980330470567,27.7881256696583,28.2743338823081),.UNSPECIFIED.);
#1995=B_SPLINE_CURVE_WITH_KNOTS('',3,(#14778,#14779,#14780,#14781,#14782,
#14783,#14784,#14785,#14786,#14787,#14788,#14789,#14790,#14791,#14792,#14793,
#14794),.UNSPECIFIED.,.F.,.F.,(4,1,1,1,1,1,1,1,1,1,1,1,1,1,4),(21.9911485751286,
22.0374712866519,22.5275639092535,23.0176565318551,23.5077491544567,23.9978417770583,
24.4879343996599,24.9780270222615,25.4681196448631,25.9582122674647,26.4483048900663,
26.9383975126679,27.4284901352695,27.9185827578711,28.2743338823081),
 .UNSPECIFIED.);
#1996=B_SPLINE_CURVE_WITH_KNOTS('',3,(#14799,#14800,#14801,#14802,#14803,
#14804,#14805,#14806,#14807,#14808,#14809,#14810,#14811,#14812,#14813,#14814,
#14815),.UNSPECIFIED.,.F.,.F.,(4,1,1,1,1,1,1,1,1,1,1,1,1,1,4),(15.707963267949,
16.02590272722,16.5159953498216,17.0060879724232,17.4961805950248,17.9862732176264,
18.476365840228,18.9664584628296,19.4565510854312,19.9466437080328,20.4367363306344,
20.926828953236,21.4169215758376,21.9070141984391,21.9911485751285),
 .UNSPECIFIED.);
#1997=B_SPLINE_CURVE_WITH_KNOTS('',3,(#14816,#14817,#14818,#14819,#14820,
#14821,#14822,#14823,#14824,#14825,#14826,#14827,#14828,#14829,#14830,#14831),
 .UNSPECIFIED.,.F.,.F.,(4,1,1,1,1,1,1,1,1,1,1,1,1,4),(15.707963267949,16.1563598154328,
16.6464524380344,17.136545060636,17.6266376832376,18.1167303058392,18.6068229284408,
19.0969155510424,19.587008173644,20.0771007962456,20.5671934188472,21.0572860414487,
21.5473786640503,21.9911485751286),.UNSPECIFIED.);
#1998=B_SPLINE_CURVE_WITH_KNOTS('',3,(#15149,#15150,#15151,#15152,#15153,
#15154,#15155,#15156,#15157,#15158,#15159,#15160,#15161,#15162,#15163,#15164,
#15165,#15166,#15167,#15168,#15169,#15170,#15171,#15172,#15173,#15174,#15175,
#15176,#15177,#15178,#15179,#15180,#15181,#15182,#15183,#15184,#15185,#15186,
#15187,#15188,#15189,#15190,#15191,#15192,#15193,#15194,#15195,#15196,#15197,
#15198,#15199,#15200,#15201,#15202,#15203,#15204,#15205,#15206,#15207,#15208,
#15209,#15210,#15211,#15212,#15213,#15214,#15215,#15216,#15217,#15218,#15219,
#15220,#15221,#15222,#15223,#15224,#15225,#15226,#15227,#15228,#15229,#15230,
#15231,#15232,#15233,#15234,#15235,#15236,#15237,#15238,#15239,#15240,#15241,
#15242,#15243,#15244,#15245,#15246,#15247,#15248,#15249,#15250,#15251,#15252,
#15253,#15254,#15255,#15256,#15257,#15258,#15259,#15260,#15261,#15262,#15263,
#15264,#15265,#15266),.UNSPECIFIED.,.F.,.F.,(4,3,3,3,3,3,3,3,3,3,3,3,3,
3,3,3,3,3,3,3,3,3,3,3,3,3,3,3,3,3,3,3,3,3,3,3,3,3,3,4),(-0.844212290556747,
-0.810702516157805,-0.79964270029283,-0.765919058559404,-0.74366337577556,
-0.731523639816212,-0.726514248567387,-0.691854085497703,-0.658890756431271,
-0.626284026666266,-0.621345574606071,-0.617273921855323,-0.587873596288652,
-0.555368241117901,-0.522812249480479,-0.490470932706205,-0.463805273987372,
-0.457610503699064,-0.453861600002129,-0.422127751490738,-0.390594093312638,
-0.383808297830876,-0.35202939501847,-0.320473779186617,-0.303891190705963,
-0.300021989550331,-0.296270020852446,-0.265284115169516,-0.234382559785099,
-0.203906579402215,-0.187813071341382,-0.164336437423709,-0.154065410084727,
-0.148511188072182,-0.144961719969282,-0.114842428131466,-0.08467071113935,
-0.0547168723966001,-0.025375144198552,0.),.UNSPECIFIED.);
#1999=B_SPLINE_CURVE_WITH_KNOTS('',3,(#15267,#15268,#15269,#15270,#15271,
#15272,#15273,#15274,#15275,#15276,#15277,#15278,#15279,#15280,#15281,#15282,
#15283,#15284,#15285),.UNSPECIFIED.,.F.,.F.,(4,3,3,3,3,3,4),(32.5258266428601,
32.8362057143071,33.3262983369087,33.8163909595103,34.3064835821119,34.7965762047135,
35.1858377202057),.UNSPECIFIED.);
#2000=B_SPLINE_CURVE_WITH_KNOTS('',3,(#15287,#15288,#15289,#15290,#15291,
#15292,#15293,#15294,#15295,#15296,#15297,#15298,#15299,#15300,#15301,#15302,
#15303,#15304,#15305,#15306,#15307,#15308,#15309,#15310,#15311,#15312,#15313,
#15314,#15315,#15316,#15317,#15318,#15319,#15320,#15321,#15322,#15323,#15324,
#15325,#15326,#15327,#15328,#15329,#15330,#15331,#15332,#15333,#15334,#15335,
#15336,#15337,#15338,#15339,#15340,#15341,#15342,#15343,#15344,#15345,#15346,
#15347,#15348,#15349,#15350,#15351,#15352,#15353,#15354,#15355,#15356,#15357,
#15358,#15359,#15360,#15361,#15362,#15363,#15364,#15365,#15366,#15367,#15368,
#15369,#15370,#15371,#15372,#15373,#15374,#15375,#15376,#15377,#15378,#15379,
#15380,#15381,#15382,#15383,#15384,#15385,#15386,#15387,#15388,#15389,#15390,
#15391,#15392,#15393,#15394,#15395,#15396,#15397,#15398,#15399,#15400,#15401,
#15402,#15403,#15404),.UNSPECIFIED.,.F.,.F.,(4,3,3,3,3,3,3,3,3,3,3,3,3,
3,3,3,3,3,3,3,3,3,3,3,3,3,3,3,3,3,3,3,3,3,3,3,3,3,3,4),(0.,0.0300123333223647,
0.037944150695711,0.067648175262101,0.097699819048293,0.127901365024015,
0.14035318466012,0.145834882567896,0.149682014312836,0.180339090874683,
0.211336159587801,0.227515922112858,0.258328578058299,0.279183136595314,
0.297430875315202,0.302279216021489,0.33366950401744,0.365348220132565,
0.397119184767528,0.425165046354417,0.450865820177805,0.4562230243213,0.459845019664696,
0.491563428307749,0.52375659439166,0.556312891291814,0.588829688145416,
0.609800462543468,0.616688207028659,0.62066244680986,0.63077123694152,0.663389038839408,
0.696389124596628,0.714867020341643,0.72933984329808,0.734034406103895,
0.767602826667506,0.801324953467599,0.834922838602097,0.844212290556745),
 .UNSPECIFIED.);
#2001=B_SPLINE_CURVE_WITH_KNOTS('',3,(#15405,#15406,#15407,#15408,#15409,
#15410,#15411,#15412,#15413,#15414,#15415,#15416,#15417,#15418,#15419),
 .UNSPECIFIED.,.F.,.F.,(4,1,1,1,1,1,1,1,1,1,1,1,4),(10.3760794513229,10.7653409668152,
11.2554335894168,11.7455262120184,12.23561883462,12.7257114572216,13.2158040798232,
13.7058967024248,14.1959893250264,14.686081947628,15.1761745702296,15.6662671928312,
15.707963267949),.UNSPECIFIED.);
#2002=B_SPLINE_CURVE_WITH_KNOTS('',3,(#15423,#15424,#15425,#15426,#15427,
#15428,#15429,#15430,#15431,#15432,#15433,#15434),.UNSPECIFIED.,.F.,.F.,
(4,1,1,1,1,1,1,1,1,4),(11.6150691238056,12.1051617464072,12.5952543690088,
13.0853469916104,13.575439614212,14.0655322368136,14.5556248594152,15.0457174820168,
15.5358101046184,15.707963267949),.UNSPECIFIED.);
#2003=B_SPLINE_CURVE_WITH_KNOTS('',3,(#15752,#15753,#15754,#15755,#15756,
#15757,#15758,#15759,#15760,#15761,#15762,#15763,#15764,#15765,#15766,#15767,
#15768,#15769,#15770,#15771,#15772,#15773,#15774,#15775,#15776,#15777,#15778,
#15779,#15780,#15781,#15782,#15783,#15784,#15785,#15786,#15787,#15788,#15789,
#15790,#15791,#15792,#15793,#15794,#15795,#15796,#15797,#15798,#15799,#15800,
#15801,#15802,#15803,#15804,#15805,#15806,#15807,#15808,#15809,#15810,#15811,
#15812,#15813,#15814,#15815,#15816,#15817,#15818,#15819,#15820,#15821,#15822,
#15823,#15824,#15825,#15826,#15827,#15828,#15829,#15830,#15831,#15832,#15833,
#15834,#15835,#15836,#15837,#15838,#15839,#15840,#15841,#15842,#15843,#15844,
#15845,#15846,#15847,#15848,#15849,#15850,#15851,#15852,#15853,#15854,#15855,
#15856,#15857,#15858,#15859,#15860,#15861,#15862,#15863,#15864,#15865,#15866),
 .UNSPECIFIED.,.F.,.F.,(4,3,3,3,3,3,3,3,3,3,3,3,3,3,3,3,3,3,3,3,3,3,3,3,
3,3,3,3,3,3,3,3,3,3,3,3,3,3,4),(-0.847325527525887,-0.817174099062059,-0.809288442555136,
-0.779387793163181,-0.759391304785787,-0.749759381505324,-0.745433732408388,
-0.713929270842299,-0.683194914240082,-0.651305400192057,-0.64722148049575,
-0.619415886144032,-0.588655017110779,-0.557502684196823,-0.526148419840108,
-0.499868882928017,-0.495563318542414,-0.491909397242946,-0.460075674578441,
-0.427928427987543,-0.421030272191743,-0.389124013627929,-0.357018072660473,
-0.339205138860963,-0.335445901760091,-0.331555114265235,-0.298995857778172,
-0.266153422414382,-0.233231717588429,-0.214514602264393,-0.187700276981344,
-0.17596900967001,-0.170411920862904,-0.166565393534998,-0.133649950991215,
-0.100083272956281,-0.0663782103294436,-0.0328789002448827,0.),
 .UNSPECIFIED.);
#2004=B_SPLINE_CURVE_WITH_KNOTS('',3,(#15867,#15868,#15869,#15870,#15871,
#15872,#15873,#15874,#15875,#15876,#15877,#15878,#15879,#15880,#15881,#15882,
#15883,#15884,#15885,#15886,#15887,#15888,#15889,#15890,#15891,#15892,#15893,
#15894,#15895,#15896,#15897,#15898,#15899,#15900,#15901,#15902,#15903,#15904,
#15905,#15906,#15907,#15908,#15909,#15910,#15911,#15912,#15913,#15914,#15915,
#15916,#15917,#15918,#15919,#15920,#15921,#15922,#15923,#15924,#15925,#15926,
#15927,#15928,#15929,#15930,#15931,#15932,#15933,#15934,#15935,#15936,#15937,
#15938,#15939,#15940,#15941,#15942,#15943,#15944,#15945,#15946,#15947,#15948,
#15949,#15950,#15951,#15952,#15953,#15954,#15955,#15956,#15957,#15958,#15959,
#15960,#15961,#15962,#15963,#15964,#15965,#15966,#15967,#15968,#15969,#15970,
#15971,#15972,#15973,#15974,#15975,#15976,#15977,#15978,#15979,#15980,#15981,
#15982,#15983,#15984),.UNSPECIFIED.,.F.,.F.,(4,3,3,3,3,3,3,3,3,3,3,3,3,
3,3,3,3,3,3,3,3,3,3,3,3,3,3,3,3,3,3,3,3,3,3,3,3,3,3,4),(0.,0.0335918750467964,
0.0447567410947651,0.0784369868399077,0.112112469599625,0.145519061555296,
0.159542948288381,0.168194038831209,0.172781428939712,0.205672698986681,
0.238354352518147,0.257710155419976,0.290609738695869,0.323232443047843,
0.333001221767483,0.337747248940037,0.36989025535088,0.401969735275938,
0.433590777177308,0.462539571533553,0.487114992308667,0.492221114477958,
0.497620252043672,0.528870508315497,0.561438615670238,0.592551446157557,
0.623302493496337,0.641222715615399,0.647822694022932,0.652667114174829,
0.65914293773446,0.689868853330734,0.720585825371081,0.736428288140424,
0.748930866867351,0.752874528704484,0.783020499126383,0.812949359166843,
0.842371062577774,0.847325527525827),.UNSPECIFIED.);
#2005=B_SPLINE_CURVE_WITH_KNOTS('',3,(#15985,#15986,#15987,#15988,#15989,
#15990,#15991,#15992,#15993,#15994,#15995,#15996,#15997),.UNSPECIFIED.,
 .F.,.F.,(4,3,3,3,4),(-37.2470393177215,-36.7569466951199,-36.2668540725183,
-35.7767614499167,-35.5088206800413),.UNSPECIFIED.);
#2451=LINE('',#14172,#3029);
#2452=LINE('',#14205,#3030);
#2453=LINE('',#14295,#3031);
#2454=LINE('',#14379,#3032);
#2455=LINE('',#14469,#3033);
#2456=LINE('',#14559,#3034);
#2457=LINE('',#14649,#3035);
#2458=LINE('',#14685,#3036);
#2459=LINE('',#14723,#3037);
#2460=LINE('',#14761,#3038);
#2461=LINE('',#14798,#3039);
#2462=LINE('',#16005,#3040);
#2463=LINE('',#16013,#3041);
#3029=VECTOR('',#10980,9.);
#3030=VECTOR('',#10985,9.);
#3031=VECTOR('',#10988,9.);
#3032=VECTOR('',#10991,9.);
#3033=VECTOR('',#10994,9.);
#3034=VECTOR('',#10997,9.);
#3035=VECTOR('',#11000,7.4455);
#3036=VECTOR('',#11005,7.4455);
#3037=VECTOR('',#11008,7.4455);
#3038=VECTOR('',#11011,7.4455);
#3039=VECTOR('',#11014,7.4455);
#3040=VECTOR('',#11029,11.);
#3041=VECTOR('',#11040,7.);
#3670=VERTEX_POINT('',#14170);
#3671=VERTEX_POINT('',#14171);
#3672=VERTEX_POINT('',#14173);
#3673=VERTEX_POINT('',#14190);
#3674=VERTEX_POINT('',#14203);
#3675=VERTEX_POINT('',#14204);
#3676=VERTEX_POINT('',#14293);
#3677=VERTEX_POINT('',#14294);
#3678=VERTEX_POINT('',#14377);
#3679=VERTEX_POINT('',#14378);
#3680=VERTEX_POINT('',#14467);
#3681=VERTEX_POINT('',#14468);
#3682=VERTEX_POINT('',#14557);
#3683=VERTEX_POINT('',#14558);
#3684=VERTEX_POINT('',#14647);
#3685=VERTEX_POINT('',#14648);
#3686=VERTEX_POINT('',#14650);
#3687=VERTEX_POINT('',#14667);
#3688=VERTEX_POINT('',#14683);
#3689=VERTEX_POINT('',#14684);
#3690=VERTEX_POINT('',#14721);
#3691=VERTEX_POINT('',#14722);
#3692=VERTEX_POINT('',#14759);
#3693=VERTEX_POINT('',#14760);
#3694=VERTEX_POINT('',#14796);
#3695=VERTEX_POINT('',#14797);
#3696=VERTEX_POINT('',#15148);
#3697=VERTEX_POINT('',#15286);
#3698=VERTEX_POINT('',#15421);
#3699=VERTEX_POINT('',#15751);
#3700=VERTEX_POINT('',#15999);
#3701=VERTEX_POINT('',#16003);
#3702=VERTEX_POINT('',#16007);
#3703=VERTEX_POINT('',#16010);
#4714=EDGE_CURVE('',#3670,#3671,#2451,.T.);
#4715=EDGE_CURVE('',#3670,#3672,#1976,.T.);
#4716=EDGE_CURVE('',#3672,#3673,#1810,.T.);
#4717=EDGE_CURVE('',#3673,#3671,#1977,.T.);
#4718=EDGE_CURVE('',#3674,#3675,#2452,.T.);
#4719=EDGE_CURVE('',#3674,#3670,#1978,.T.);
#4720=EDGE_CURVE('',#3671,#3675,#1979,.T.);
#4721=EDGE_CURVE('',#3676,#3677,#2453,.T.);
#4722=EDGE_CURVE('',#3676,#3674,#1980,.T.);
#4723=EDGE_CURVE('',#3675,#3677,#1981,.T.);
#4724=EDGE_CURVE('',#3678,#3679,#2454,.T.);
#4725=EDGE_CURVE('',#3678,#3676,#1982,.T.);
#4726=EDGE_CURVE('',#3677,#3679,#1983,.T.);
#4727=EDGE_CURVE('',#3680,#3681,#2455,.T.);
#4728=EDGE_CURVE('',#3680,#3678,#1984,.T.);
#4729=EDGE_CURVE('',#3679,#3681,#1985,.T.);
#4730=EDGE_CURVE('',#3682,#3683,#2456,.T.);
#4731=EDGE_CURVE('',#3682,#3680,#1986,.T.);
#4732=EDGE_CURVE('',#3681,#3683,#1987,.T.);
#4733=EDGE_CURVE('',#3684,#3685,#2457,.T.);
#4734=EDGE_CURVE('',#3684,#3686,#1988,.T.);
#4735=EDGE_CURVE('',#3687,#3686,#1811,.T.);
#4736=EDGE_CURVE('',#3685,#3687,#1989,.T.);
#4737=EDGE_CURVE('',#3688,#3689,#2458,.T.);
#4738=EDGE_CURVE('',#3688,#3684,#1990,.T.);
#4739=EDGE_CURVE('',#3689,#3685,#1991,.T.);
#4740=EDGE_CURVE('',#3690,#3691,#2459,.T.);
#4741=EDGE_CURVE('',#3690,#3688,#1992,.T.);
#4742=EDGE_CURVE('',#3691,#3689,#1993,.T.);
#4743=EDGE_CURVE('',#3692,#3693,#2460,.T.);
#4744=EDGE_CURVE('',#3692,#3690,#1994,.T.);
#4745=EDGE_CURVE('',#3693,#3691,#1995,.T.);
#4746=EDGE_CURVE('',#3694,#3695,#2461,.T.);
#4747=EDGE_CURVE('',#3694,#3692,#1996,.T.);
#4748=EDGE_CURVE('',#3695,#3693,#1997,.T.);
#4749=EDGE_CURVE('',#3696,#3687,#1998,.T.);
#4750=EDGE_CURVE('',#3683,#3696,#1999,.T.);
#4751=EDGE_CURVE('',#3697,#3673,#2000,.T.);
#4752=EDGE_CURVE('',#3697,#3695,#2001,.T.);
#4753=EDGE_CURVE('',#3698,#3697,#1812,.T.);
#4754=EDGE_CURVE('',#3698,#3694,#2002,.T.);
#4755=EDGE_CURVE('',#3686,#3699,#2003,.T.);
#4756=EDGE_CURVE('',#3672,#3698,#2004,.T.);
#4757=EDGE_CURVE('',#3699,#3682,#2005,.T.);
#4758=EDGE_CURVE('',#3700,#3700,#1813,.T.);
#4759=EDGE_CURVE('',#3699,#3696,#1814,.T.);
#4760=EDGE_CURVE('',#3701,#3701,#1815,.T.);
#4761=EDGE_CURVE('',#3701,#3700,#2462,.T.);
#4762=EDGE_CURVE('',#3702,#3702,#1816,.T.);
#4763=EDGE_CURVE('',#3703,#3703,#1817,.T.);
#4764=EDGE_CURVE('',#3702,#3703,#2463,.T.);
#6693=ORIENTED_EDGE('',*,*,#4714,.F.);
#6694=ORIENTED_EDGE('',*,*,#4715,.T.);
#6695=ORIENTED_EDGE('',*,*,#4716,.T.);
#6696=ORIENTED_EDGE('',*,*,#4717,.T.);
#6697=ORIENTED_EDGE('',*,*,#4718,.F.);
#6698=ORIENTED_EDGE('',*,*,#4719,.T.);
#6699=ORIENTED_EDGE('',*,*,#4714,.T.);
#6700=ORIENTED_EDGE('',*,*,#4720,.T.);
#6701=ORIENTED_EDGE('',*,*,#4721,.F.);
#6702=ORIENTED_EDGE('',*,*,#4722,.T.);
#6703=ORIENTED_EDGE('',*,*,#4718,.T.);
#6704=ORIENTED_EDGE('',*,*,#4723,.T.);
#6705=ORIENTED_EDGE('',*,*,#4724,.F.);
#6706=ORIENTED_EDGE('',*,*,#4725,.T.);
#6707=ORIENTED_EDGE('',*,*,#4721,.T.);
#6708=ORIENTED_EDGE('',*,*,#4726,.T.);
#6709=ORIENTED_EDGE('',*,*,#4727,.F.);
#6710=ORIENTED_EDGE('',*,*,#4728,.T.);
#6711=ORIENTED_EDGE('',*,*,#4724,.T.);
#6712=ORIENTED_EDGE('',*,*,#4729,.T.);
#6713=ORIENTED_EDGE('',*,*,#4730,.F.);
#6714=ORIENTED_EDGE('',*,*,#4731,.T.);
#6715=ORIENTED_EDGE('',*,*,#4727,.T.);
#6716=ORIENTED_EDGE('',*,*,#4732,.T.);
#6717=ORIENTED_EDGE('',*,*,#4733,.F.);
#6718=ORIENTED_EDGE('',*,*,#4734,.T.);
#6719=ORIENTED_EDGE('',*,*,#4735,.F.);
#6720=ORIENTED_EDGE('',*,*,#4736,.F.);
#6721=ORIENTED_EDGE('',*,*,#4737,.F.);
#6722=ORIENTED_EDGE('',*,*,#4738,.T.);
#6723=ORIENTED_EDGE('',*,*,#4733,.T.);
#6724=ORIENTED_EDGE('',*,*,#4739,.F.);
#6725=ORIENTED_EDGE('',*,*,#4740,.F.);
#6726=ORIENTED_EDGE('',*,*,#4741,.T.);
#6727=ORIENTED_EDGE('',*,*,#4737,.T.);
#6728=ORIENTED_EDGE('',*,*,#4742,.F.);
#6729=ORIENTED_EDGE('',*,*,#4743,.F.);
#6730=ORIENTED_EDGE('',*,*,#4744,.T.);
#6731=ORIENTED_EDGE('',*,*,#4740,.T.);
#6732=ORIENTED_EDGE('',*,*,#4745,.F.);
#6733=ORIENTED_EDGE('',*,*,#4746,.F.);
#6734=ORIENTED_EDGE('',*,*,#4747,.T.);
#6735=ORIENTED_EDGE('',*,*,#4743,.T.);
#6736=ORIENTED_EDGE('',*,*,#4748,.F.);
#6737=ORIENTED_EDGE('',*,*,#4749,.F.);
#6738=ORIENTED_EDGE('',*,*,#4750,.F.);
#6739=ORIENTED_EDGE('',*,*,#4732,.F.);
#6740=ORIENTED_EDGE('',*,*,#4729,.F.);
#6741=ORIENTED_EDGE('',*,*,#4726,.F.);
#6742=ORIENTED_EDGE('',*,*,#4723,.F.);
#6743=ORIENTED_EDGE('',*,*,#4720,.F.);
#6744=ORIENTED_EDGE('',*,*,#4717,.F.);
#6745=ORIENTED_EDGE('',*,*,#4751,.F.);
#6746=ORIENTED_EDGE('',*,*,#4752,.T.);
#6747=ORIENTED_EDGE('',*,*,#4748,.T.);
#6748=ORIENTED_EDGE('',*,*,#4745,.T.);
#6749=ORIENTED_EDGE('',*,*,#4742,.T.);
#6750=ORIENTED_EDGE('',*,*,#4739,.T.);
#6751=ORIENTED_EDGE('',*,*,#4736,.T.);
#6752=ORIENTED_EDGE('',*,*,#4746,.T.);
#6753=ORIENTED_EDGE('',*,*,#4752,.F.);
#6754=ORIENTED_EDGE('',*,*,#4753,.F.);
#6755=ORIENTED_EDGE('',*,*,#4754,.T.);
#6756=ORIENTED_EDGE('',*,*,#4755,.F.);
#6757=ORIENTED_EDGE('',*,*,#4734,.F.);
#6758=ORIENTED_EDGE('',*,*,#4738,.F.);
#6759=ORIENTED_EDGE('',*,*,#4741,.F.);
#6760=ORIENTED_EDGE('',*,*,#4744,.F.);
#6761=ORIENTED_EDGE('',*,*,#4747,.F.);
#6762=ORIENTED_EDGE('',*,*,#4754,.F.);
#6763=ORIENTED_EDGE('',*,*,#4756,.F.);
#6764=ORIENTED_EDGE('',*,*,#4715,.F.);
#6765=ORIENTED_EDGE('',*,*,#4719,.F.);
#6766=ORIENTED_EDGE('',*,*,#4722,.F.);
#6767=ORIENTED_EDGE('',*,*,#4725,.F.);
#6768=ORIENTED_EDGE('',*,*,#4728,.F.);
#6769=ORIENTED_EDGE('',*,*,#4731,.F.);
#6770=ORIENTED_EDGE('',*,*,#4757,.F.);
#6771=ORIENTED_EDGE('',*,*,#4758,.F.);
#6772=ORIENTED_EDGE('',*,*,#4759,.T.);
#6773=ORIENTED_EDGE('',*,*,#4749,.T.);
#6774=ORIENTED_EDGE('',*,*,#4735,.T.);
#6775=ORIENTED_EDGE('',*,*,#4755,.T.);
#6776=ORIENTED_EDGE('',*,*,#4760,.F.);
#6777=ORIENTED_EDGE('',*,*,#4761,.T.);
#6778=ORIENTED_EDGE('',*,*,#4758,.T.);
#6779=ORIENTED_EDGE('',*,*,#4761,.F.);
#6780=ORIENTED_EDGE('',*,*,#4760,.T.);
#6781=ORIENTED_EDGE('',*,*,#4762,.T.);
#6782=ORIENTED_EDGE('',*,*,#4751,.T.);
#6783=ORIENTED_EDGE('',*,*,#4716,.F.);
#6784=ORIENTED_EDGE('',*,*,#4756,.T.);
#6785=ORIENTED_EDGE('',*,*,#4753,.T.);
#6786=ORIENTED_EDGE('',*,*,#4763,.F.);
#6787=ORIENTED_EDGE('',*,*,#4762,.F.);
#6788=ORIENTED_EDGE('',*,*,#4764,.T.);
#6789=ORIENTED_EDGE('',*,*,#4763,.T.);
#6790=ORIENTED_EDGE('',*,*,#4764,.F.);
#6791=ORIENTED_EDGE('',*,*,#4730,.T.);
#6792=ORIENTED_EDGE('',*,*,#4750,.T.);
#6793=ORIENTED_EDGE('',*,*,#4759,.F.);
#6794=ORIENTED_EDGE('',*,*,#4757,.T.);
#7583=CYLINDRICAL_SURFACE('',#8909,8.866);
#7584=CYLINDRICAL_SURFACE('',#8911,8.866);
#7585=CYLINDRICAL_SURFACE('',#8912,8.866);
#7586=CYLINDRICAL_SURFACE('',#8913,8.866);
#7587=CYLINDRICAL_SURFACE('',#8914,8.866);
#7588=CYLINDRICAL_SURFACE('',#8915,8.866);
#7589=CYLINDRICAL_SURFACE('',#8916,7.4455);
#7590=CYLINDRICAL_SURFACE('',#8918,7.4455);
#7591=CYLINDRICAL_SURFACE('',#8919,7.4455);
#7592=CYLINDRICAL_SURFACE('',#8920,7.4455);
#7593=CYLINDRICAL_SURFACE('',#8921,7.4455);
#7594=CYLINDRICAL_SURFACE('',#8922,7.4455);
#7595=CYLINDRICAL_SURFACE('',#8927,11.);
#7596=CYLINDRICAL_SURFACE('',#8933,7.);
#7597=CYLINDRICAL_SURFACE('',#8934,8.866);
#7964=ADVANCED_FACE('',(#802),#7583,.T.);
#7965=ADVANCED_FACE('',(#803),#7584,.T.);
#7966=ADVANCED_FACE('',(#804),#7585,.T.);
#7967=ADVANCED_FACE('',(#805),#7586,.T.);
#7968=ADVANCED_FACE('',(#806),#7587,.T.);
#7969=ADVANCED_FACE('',(#807),#7588,.T.);
#7970=ADVANCED_FACE('',(#808),#7589,.T.);
#7971=ADVANCED_FACE('',(#809),#7590,.T.);
#7972=ADVANCED_FACE('',(#810),#7591,.T.);
#7973=ADVANCED_FACE('',(#811),#7592,.T.);
#7974=ADVANCED_FACE('',(#812),#7593,.T.);
#7975=ADVANCED_FACE('',(#813),#84,.F.);
#7976=ADVANCED_FACE('',(#814),#7594,.T.);
#7977=ADVANCED_FACE('',(#815),#85,.F.);
#7978=ADVANCED_FACE('',(#816,#168),#402,.T.);
#7979=ADVANCED_FACE('',(#817),#7595,.T.);
#7980=ADVANCED_FACE('',(#818,#169),#403,.F.);
#7981=ADVANCED_FACE('',(#819,#170),#404,.T.);
#7982=ADVANCED_FACE('',(#820),#7596,.F.);
#7983=ADVANCED_FACE('',(#821),#7597,.T.);
#8121=CLOSED_SHELL('',(#7964,#7965,#7966,#7967,#7968,#7969,#7970,#7971,
#7972,#7973,#7974,#7975,#7976,#7977,#7978,#7979,#7980,#7981,#7982,#7983));
#8908=AXIS2_PLACEMENT_3D('',#14168,#10976,#10977);
#8909=AXIS2_PLACEMENT_3D('',#14169,#10978,#10979);
#8910=AXIS2_PLACEMENT_3D('',#14191,#10981,#10982);
#8911=AXIS2_PLACEMENT_3D('',#14202,#10983,#10984);
#8912=AXIS2_PLACEMENT_3D('',#14292,#10986,#10987);
#8913=AXIS2_PLACEMENT_3D('',#14376,#10989,#10990);
#8914=AXIS2_PLACEMENT_3D('',#14466,#10992,#10993);
#8915=AXIS2_PLACEMENT_3D('',#14556,#10995,#10996);
#8916=AXIS2_PLACEMENT_3D('',#14646,#10998,#10999);
#8917=AXIS2_PLACEMENT_3D('',#14668,#11001,#11002);
#8918=AXIS2_PLACEMENT_3D('',#14682,#11003,#11004);
#8919=AXIS2_PLACEMENT_3D('',#14720,#11006,#11007);
#8920=AXIS2_PLACEMENT_3D('',#14758,#11009,#11010);
#8921=AXIS2_PLACEMENT_3D('',#14795,#11012,#11013);
#8922=AXIS2_PLACEMENT_3D('',#15420,#11015,#11016);
#8923=AXIS2_PLACEMENT_3D('',#15422,#11017,#11018);
#8924=AXIS2_PLACEMENT_3D('',#15998,#11019,#11020);
#8925=AXIS2_PLACEMENT_3D('',#16000,#11021,#11022);
#8926=AXIS2_PLACEMENT_3D('',#16001,#11023,#11024);
#8927=AXIS2_PLACEMENT_3D('',#16002,#11025,#11026);
#8928=AXIS2_PLACEMENT_3D('',#16004,#11027,#11028);
#8929=AXIS2_PLACEMENT_3D('',#16006,#11030,#11031);
#8930=AXIS2_PLACEMENT_3D('',#16008,#11032,#11033);
#8931=AXIS2_PLACEMENT_3D('',#16009,#11034,#11035);
#8932=AXIS2_PLACEMENT_3D('',#16011,#11036,#11037);
#8933=AXIS2_PLACEMENT_3D('',#16012,#11038,#11039);
#8934=AXIS2_PLACEMENT_3D('',#16014,#11041,#11042);
#10976=DIRECTION('axis',(0.,0.,1.));
#10977=DIRECTION('refdir',(1.,0.,0.));
#10978=DIRECTION('center_axis',(0.,0.,-1.));
#10979=DIRECTION('ref_axis',(1.,0.,0.));
#10980=DIRECTION('',(0.,0.,1.));
#10981=DIRECTION('center_axis',(0.,0.,-1.));
#10982=DIRECTION('ref_axis',(1.,0.,0.));
#10983=DIRECTION('center_axis',(0.,0.,-1.));
#10984=DIRECTION('ref_axis',(1.,0.,0.));
#10985=DIRECTION('',(0.,0.,1.));
#10986=DIRECTION('center_axis',(0.,0.,-1.));
#10987=DIRECTION('ref_axis',(1.,0.,0.));
#10988=DIRECTION('',(0.,0.,1.));
#10989=DIRECTION('center_axis',(0.,0.,-1.));
#10990=DIRECTION('ref_axis',(1.,0.,0.));
#10991=DIRECTION('',(0.,0.,1.));
#10992=DIRECTION('center_axis',(0.,0.,-1.));
#10993=DIRECTION('ref_axis',(1.,0.,0.));
#10994=DIRECTION('',(0.,0.,1.));
#10995=DIRECTION('center_axis',(0.,0.,-1.));
#10996=DIRECTION('ref_axis',(1.,0.,0.));
#10997=DIRECTION('',(0.,0.,1.));
#10998=DIRECTION('center_axis',(0.,0.,-1.));
#10999=DIRECTION('ref_axis',(0.986989031429609,0.160787598519419,0.));
#11000=DIRECTION('',(0.,0.,-1.));
#11001=DIRECTION('center_axis',(0.,0.,-1.));
#11002=DIRECTION('ref_axis',(1.,-4.52218161043494E-15,0.));
#11003=DIRECTION('center_axis',(0.,0.,-1.));
#11004=DIRECTION('ref_axis',(1.,-4.52218161043494E-15,0.));
#11005=DIRECTION('',(0.,0.,-1.));
#11006=DIRECTION('center_axis',(0.,0.,-1.));
#11007=DIRECTION('ref_axis',(1.,-4.52218161043494E-15,0.));
#11008=DIRECTION('',(0.,0.,-1.));
#11009=DIRECTION('center_axis',(0.,0.,-1.));
#11010=DIRECTION('ref_axis',(1.,-4.52218161043494E-15,0.));
#11011=DIRECTION('',(0.,0.,-1.));
#11012=DIRECTION('center_axis',(0.,0.,-1.));
#11013=DIRECTION('ref_axis',(1.,-4.52218161043494E-15,0.));
#11014=DIRECTION('',(0.,0.,-1.));
#11015=DIRECTION('center_axis',(0.,0.,-1.));
#11016=DIRECTION('ref_axis',(1.,-4.52218161043494E-15,0.));
#11017=DIRECTION('center_axis',(0.,0.,1.));
#11018=DIRECTION('ref_axis',(1.,-4.52218161043494E-15,0.));
#11019=DIRECTION('center_axis',(0.,0.,1.));
#11020=DIRECTION('ref_axis',(1.,0.,0.));
#11021=DIRECTION('center_axis',(0.,0.,-1.));
#11022=DIRECTION('ref_axis',(1.,0.,0.));
#11023=DIRECTION('center_axis',(0.,0.,-1.));
#11024=DIRECTION('ref_axis',(1.,0.,0.));
#11025=DIRECTION('center_axis',(0.,0.,-1.));
#11026=DIRECTION('ref_axis',(1.,0.,0.));
#11027=DIRECTION('center_axis',(0.,0.,-1.));
#11028=DIRECTION('ref_axis',(1.,0.,0.));
#11029=DIRECTION('',(0.,0.,1.));
#11030=DIRECTION('center_axis',(0.,0.,1.));
#11031=DIRECTION('ref_axis',(1.,0.,0.));
#11032=DIRECTION('center_axis',(0.,0.,1.));
#11033=DIRECTION('ref_axis',(1.,0.,0.));
#11034=DIRECTION('center_axis',(0.,0.,1.));
#11035=DIRECTION('ref_axis',(1.,0.,0.));
#11036=DIRECTION('center_axis',(0.,0.,1.));
#11037=DIRECTION('ref_axis',(1.,0.,0.));
#11038=DIRECTION('center_axis',(0.,0.,-1.));
#11039=DIRECTION('ref_axis',(1.,0.,0.));
#11040=DIRECTION('',(0.,0.,1.));
#11041=DIRECTION('center_axis',(0.,0.,-1.));
#11042=DIRECTION('ref_axis',(-0.23846786087739,0.971150389655774,0.));
#14168=CARTESIAN_POINT('',(0.,0.,0.));
#14169=CARTESIAN_POINT('Origin',(-6.5,6.43177298256785,260.886209595194));
#14170=CARTESIAN_POINT('',(-15.3655563966863,6.43160863162147,258.077824816097));
#14171=CARTESIAN_POINT('',(-15.3658820331401,6.43164402321515,258.444594374291));
#14172=CARTESIAN_POINT('',(-15.366,6.43177298256785,260.886209595194));
#14173=CARTESIAN_POINT('',(-2.55683773519921,-1.50909770983428,258.886209595194));
#14174=CARTESIAN_POINT('Ctrl Pts',(-15.3655563966863,6.43160863162147,258.077824816097));
#14175=CARTESIAN_POINT('Ctrl Pts',(-15.365908581386,5.92277029184256,258.100657338524));
#14176=CARTESIAN_POINT('Ctrl Pts',(-15.3227955907809,5.41399103993066,258.123489860952));
#14177=CARTESIAN_POINT('Ctrl Pts',(-15.2356628566919,4.91286580948705,258.146322383379));
#14178=CARTESIAN_POINT('Ctrl Pts',(-14.9876098477437,3.48624213503058,258.211322936263));
#14179=CARTESIAN_POINT('Ctrl Pts',(-14.382798754648,2.12165049027129,258.276323489146));
#14180=CARTESIAN_POINT('Ctrl Pts',(-13.4924209785142,0.979715202365416,
258.341324042029));
#14181=CARTESIAN_POINT('Ctrl Pts',(-12.6020432023805,-0.162220085540456,
258.406324594912));
#14182=CARTESIAN_POINT('Ctrl Pts',(-11.4260987432086,-1.08149901659292,
258.471325147796));
#14183=CARTESIAN_POINT('Ctrl Pts',(-10.1030119047582,-1.66990669415313,
258.536325700679));
#14184=CARTESIAN_POINT('Ctrl Pts',(-8.77992506630778,-2.25831437171335,
258.601326253562));
#14185=CARTESIAN_POINT('Ctrl Pts',(-7.30969584857881,-2.51585079578131,
258.666326806446));
#14186=CARTESIAN_POINT('Ctrl Pts',(-5.86537969542476,-2.41221435349705,
258.731327359329));
#14187=CARTESIAN_POINT('Ctrl Pts',(-4.71821552951209,-2.3298999567415,258.782954771284));
#14188=CARTESIAN_POINT('Ctrl Pts',(-3.58739863923219,-2.01973939457909,
258.834582183239));
#14189=CARTESIAN_POINT('Ctrl Pts',(-2.55659399163549,-1.50913350781768,
258.886209595194));
#14190=CARTESIAN_POINT('',(-10.4431622648008,-1.50909770983426,258.886209595194));
#14191=CARTESIAN_POINT('Origin',(-6.5,6.43177298256785,258.886209595194));
#14192=CARTESIAN_POINT('Ctrl Pts',(-10.4431622648007,-1.50909770983434,
258.886209595194));
#14193=CARTESIAN_POINT('Ctrl Pts',(-11.7404163125939,-0.86492613126773,
258.82120904231));
#14194=CARTESIAN_POINT('Ctrl Pts',(-12.8761753779444,0.10296746655448,258.756208489427));
#14195=CARTESIAN_POINT('Ctrl Pts',(-13.7172937557503,1.28146572034169,258.691207936544));
#14196=CARTESIAN_POINT('Ctrl Pts',(-14.5584121335561,2.4599639741289,258.626207383661));
#14197=CARTESIAN_POINT('Ctrl Pts',(-15.1048898238173,3.84906688388111,258.561206830778));
#14198=CARTESIAN_POINT('Ctrl Pts',(-15.2922292071869,5.28493656649312,258.496206277894));
#14199=CARTESIAN_POINT('Ctrl Pts',(-15.3418131043833,5.66497419365675,258.479002310026));
#14200=CARTESIAN_POINT('Ctrl Pts',(-15.3662384939932,6.04828794644444,258.461798342159));
#14201=CARTESIAN_POINT('Ctrl Pts',(-15.3658820331401,6.43164402321515,258.444594374291));
#14202=CARTESIAN_POINT('Origin',(-6.5,6.43177298256785,260.886209595194));
#14203=CARTESIAN_POINT('',(-15.3662755781924,6.43158183962034,255.577824816097));
#14204=CARTESIAN_POINT('',(-15.3665939393721,6.43165874093672,255.944594374291));
#14205=CARTESIAN_POINT('',(-15.366,6.43177298256785,260.886209595194));
#14206=CARTESIAN_POINT('Ctrl Pts',(-15.3662755781924,6.43158183962034,255.577824816097));
#14207=CARTESIAN_POINT('Ctrl Pts',(-15.3665112565053,6.1829613866446,255.588983484375));
#14208=CARTESIAN_POINT('Ctrl Pts',(-15.3562554254084,5.93436031665608,255.600142152654));
#14209=CARTESIAN_POINT('Ctrl Pts',(-15.3353656673878,5.68665604249679,255.611300820932));
#14210=CARTESIAN_POINT('Ctrl Pts',(-15.213680374209,4.2437495620628,255.676301373815));
#14211=CARTESIAN_POINT('Ctrl Pts',(-14.7311647485395,2.83127315130671,255.741301926699));
#14212=CARTESIAN_POINT('Ctrl Pts',(-13.9446160597533,1.61549044790784,255.806302479582));
#14213=CARTESIAN_POINT('Ctrl Pts',(-13.158067370967,0.399707744508963,255.871303032465));
#14214=CARTESIAN_POINT('Ctrl Pts',(-12.067485619064,-0.619381251532671,
255.936303585348));
#14215=CARTESIAN_POINT('Ctrl Pts',(-10.8012439843536,-1.32181882492555,
256.001304138232));
#14216=CARTESIAN_POINT('Ctrl Pts',(-9.53500234964327,-2.02425639831843,
256.066304691115));
#14217=CARTESIAN_POINT('Ctrl Pts',(-8.0931008321256,-2.41004254906253,256.131305243998));
#14218=CARTESIAN_POINT('Ctrl Pts',(-6.64526672060094,-2.43376610496901,
256.196305796881));
#14219=CARTESIAN_POINT('Ctrl Pts',(-5.19743260907629,-2.45748966087549,
256.261306349765));
#14220=CARTESIAN_POINT('Ctrl Pts',(-3.74366590354462,-2.11915062194435,
256.326306902648));
#14221=CARTESIAN_POINT('Ctrl Pts',(-2.45509055196917,-1.4585751265513,256.391307455531));
#14222=CARTESIAN_POINT('Ctrl Pts',(-1.16651520039374,-0.797999631158263,
256.456308008415));
#14223=CARTESIAN_POINT('Ctrl Pts',(-0.0431312027745352,0.184812320696678,
256.521308561298));
#14224=CARTESIAN_POINT('Ctrl Pts',(0.782827082714929,1.37417321356813,256.586309114181));
#14225=CARTESIAN_POINT('Ctrl Pts',(1.6087853682044,2.5635341064396,256.651309667064));
#14226=CARTESIAN_POINT('Ctrl Pts',(2.13731794156413,3.95944394032759,256.716310219948));
#14227=CARTESIAN_POINT('Ctrl Pts',(2.30621084745112,5.39758913611839,256.781310772831));
#14228=CARTESIAN_POINT('Ctrl Pts',(2.47510375333811,6.83573433190919,256.846311325714));
#14229=CARTESIAN_POINT('Ctrl Pts',(2.28435699175236,8.31611488960281,256.911311878597));
#14230=CARTESIAN_POINT('Ctrl Pts',(1.75642349837671,9.66447413648814,256.976312431481));
#14231=CARTESIAN_POINT('Ctrl Pts',(1.22849000500107,11.0128333833735,257.041312984364));
#14232=CARTESIAN_POINT('Ctrl Pts',(0.363369779835524,12.2291713194505,257.106313537247));
#14233=CARTESIAN_POINT('Ctrl Pts',(-0.737103225919464,13.1703118853259,
257.17131409013));
#14234=CARTESIAN_POINT('Ctrl Pts',(-1.83757623167446,14.1114524512014,257.236314643014));
#14235=CARTESIAN_POINT('Ctrl Pts',(-3.1734020180189,14.7773956468752,257.301315195897));
#14236=CARTESIAN_POINT('Ctrl Pts',(-4.58733957700001,15.0897528652687,257.36631574878));
#14237=CARTESIAN_POINT('Ctrl Pts',(-6.00127713598111,15.4021100836622,257.431316301664));
#14238=CARTESIAN_POINT('Ctrl Pts',(-7.49332646759887,15.3608813247754,257.496316854547));
#14239=CARTESIAN_POINT('Ctrl Pts',(-8.88785728598738,14.9709195332554,257.56131740743));
#14240=CARTESIAN_POINT('Ctrl Pts',(-10.2823881043759,14.5809577417353,257.626317960313));
#14241=CARTESIAN_POINT('Ctrl Pts',(-11.5794004095351,13.842262917582,257.691318513197));
#14242=CARTESIAN_POINT('Ctrl Pts',(-12.626222062206,12.8417876386424,257.75631906608));
#14243=CARTESIAN_POINT('Ctrl Pts',(-13.6730437148769,11.8413123597028,257.821319618963));
#14244=CARTESIAN_POINT('Ctrl Pts',(-14.4696747150594,10.5790566259768,257.886320171846));
#14245=CARTESIAN_POINT('Ctrl Pts',(-14.9223427527502,9.20360090703698,257.951320724729));
#14246=CARTESIAN_POINT('Ctrl Pts',(-15.2160036333582,8.31129682539304,257.993488755185));
#14247=CARTESIAN_POINT('Ctrl Pts',(-15.3649059676683,7.37135195945706,258.035656785641));
#14248=CARTESIAN_POINT('Ctrl Pts',(-15.3655563966863,6.43160863162147,258.077824816097));
#14249=CARTESIAN_POINT('Ctrl Pts',(-15.3658820331401,6.43164402321515,258.444594374291));
#14250=CARTESIAN_POINT('Ctrl Pts',(-15.3648917027932,7.49669549595043,258.396797789275));
#14251=CARTESIAN_POINT('Ctrl Pts',(-15.1726210818878,8.56207364904321,258.34900120426));
#14252=CARTESIAN_POINT('Ctrl Pts',(-14.7971471860228,9.55843300974454,258.301204619244));
#14253=CARTESIAN_POINT('Ctrl Pts',(-14.286524705011,10.9134233149121,258.236204066361));
#14254=CARTESIAN_POINT('Ctrl Pts',(-13.4370786665095,12.1407674697755,258.171203513478));
#14255=CARTESIAN_POINT('Ctrl Pts',(-12.3487596071053,13.0959348658895,258.106202960595));
#14256=CARTESIAN_POINT('Ctrl Pts',(-11.2604405477011,14.0511022620034,258.041202407711));
#14257=CARTESIAN_POINT('Ctrl Pts',(-9.93324846739419,14.734092899368,257.976201854828));
#14258=CARTESIAN_POINT('Ctrl Pts',(-8.52342686227239,15.0645361066618,257.911201301945));
#14259=CARTESIAN_POINT('Ctrl Pts',(-7.11360525715061,15.3949793139555,257.846200749062));
#14260=CARTESIAN_POINT('Ctrl Pts',(-5.6211541272139,15.3728750911786,257.781200196178));
#14261=CARTESIAN_POINT('Ctrl Pts',(-4.22174266980788,15.0008133213866,257.716199643295));
#14262=CARTESIAN_POINT('Ctrl Pts',(-2.82233121240186,14.6287515515946,257.651199090412));
#14263=CARTESIAN_POINT('Ctrl Pts',(-1.51595942752651,13.9067322347875,257.586198537529));
#14264=CARTESIAN_POINT('Ctrl Pts',(-0.456405209262731,12.919750140243,257.521197984645));
#14265=CARTESIAN_POINT('Ctrl Pts',(0.603149009001058,11.9327680456984,257.456197431762));
#14266=CARTESIAN_POINT('Ctrl Pts',(1.41588566065329,10.6808231734162,257.391196878879));
#14267=CARTESIAN_POINT('Ctrl Pts',(1.88613869287802,9.31128036624651,257.326196325996));
#14268=CARTESIAN_POINT('Ctrl Pts',(2.35639172510274,7.94173755907686,257.261195773112));
#14269=CARTESIAN_POINT('Ctrl Pts',(2.48416113789998,6.45459681701972,257.196195220229));
#14270=CARTESIAN_POINT('Ctrl Pts',(2.25440627641291,5.024911711378,257.131194667346));
#14271=CARTESIAN_POINT('Ctrl Pts',(2.02465141492584,3.59522660573629,257.066194114462));
#14272=CARTESIAN_POINT('Ctrl Pts',(1.43737227915447,2.22299713651001,257.001193561579));
#14273=CARTESIAN_POINT('Ctrl Pts',(0.561698305318104,1.06974891578268,256.936193008696));
#14274=CARTESIAN_POINT('Ctrl Pts',(-0.313975668518257,-0.0834993049446531,
256.871192455813));
#14275=CARTESIAN_POINT('Ctrl Pts',(-1.47804448041961,-1.01776627717304,
256.806191902929));
#14276=CARTESIAN_POINT('Ctrl Pts',(-2.79348490795269,-1.62307850617608,
256.741191350046));
#14277=CARTESIAN_POINT('Ctrl Pts',(-4.10892533548576,-2.22839073517912,
256.676190797163));
#14278=CARTESIAN_POINT('Ctrl Pts',(-5.57573737865058,-2.50474822095681,
256.61119024428));
#14279=CARTESIAN_POINT('Ctrl Pts',(-7.02126143274018,-2.41962083214006,
256.546189691396));
#14280=CARTESIAN_POINT('Ctrl Pts',(-8.46678548682979,-2.33449344332332,
256.481189138513));
#14281=CARTESIAN_POINT('Ctrl Pts',(-9.8910215518442,-1.88788117991214,256.41618858563));
#14282=CARTESIAN_POINT('Ctrl Pts',(-11.1263217894382,-1.13235504876889,
256.351188032747));
#14283=CARTESIAN_POINT('Ctrl Pts',(-12.3616220270321,-0.37682891762563,
256.286187479863));
#14284=CARTESIAN_POINT('Ctrl Pts',(-13.4079864372057,0.687611081249703,
256.22118692698));
#14285=CARTESIAN_POINT('Ctrl Pts',(-14.1422466784471,1.93566890880313,256.156186374097));
#14286=CARTESIAN_POINT('Ctrl Pts',(-14.8765069196884,3.18372673635655,256.091185821213));
#14287=CARTESIAN_POINT('Ctrl Pts',(-15.2986629919977,4.61540239258807,256.02618526833));
#14288=CARTESIAN_POINT('Ctrl Pts',(-15.3590226012745,6.06217229347312,255.961184715447));
#14289=CARTESIAN_POINT('Ctrl Pts',(-15.3641578730301,6.18526050921736,255.955654601728));
#14290=CARTESIAN_POINT('Ctrl Pts',(-15.3666743688619,6.30845798098958,255.950124488009));
#14291=CARTESIAN_POINT('Ctrl Pts',(-15.3665939393721,6.43165874093672,255.944594374291));
#14292=CARTESIAN_POINT('Origin',(-6.5,6.43177298256785,260.886209595194));
#14293=CARTESIAN_POINT('',(-15.3667277726507,6.43178433461072,253.077824816097));
#14294=CARTESIAN_POINT('',(-15.3665655929379,6.43189805357513,253.444594374291));
#14295=CARTESIAN_POINT('',(-15.366,6.43177298256785,260.886209595194));
#14296=CARTESIAN_POINT('Ctrl Pts',(-15.3667277726507,6.43178433461072,253.077824816097));
#14297=CARTESIAN_POINT('Ctrl Pts',(-15.3666159753282,4.99523210882893,253.14231018311));
#14298=CARTESIAN_POINT('Ctrl Pts',(-15.0104403492592,3.55862641061937,253.206795550122));
#14299=CARTESIAN_POINT('Ctrl Pts',(-14.3391729900672,2.2885553244482,253.271280917135));
#14300=CARTESIAN_POINT('Ctrl Pts',(-13.662542748179,1.00833739863445,253.336281470018));
#14301=CARTESIAN_POINT('Ctrl Pts',(-12.6657660061007,-0.102674332284354,
253.401282022901));
#14302=CARTESIAN_POINT('Ctrl Pts',(-11.4661740875396,-0.913701860014089,
253.466282575784));
#14303=CARTESIAN_POINT('Ctrl Pts',(-10.2665821689785,-1.72472938774381,
253.531283128668));
#14304=CARTESIAN_POINT('Ctrl Pts',(-8.86417507393453,-2.23577271228447,
253.596283681551));
#14305=CARTESIAN_POINT('Ctrl Pts',(-7.42403117341256,-2.38667654789474,
253.661284234434));
#14306=CARTESIAN_POINT('Ctrl Pts',(-5.98388727289058,-2.537580383505,253.726284787317));
#14307=CARTESIAN_POINT('Ctrl Pts',(-4.50600656689059,-2.32834473018485,
253.791285340201));
#14308=CARTESIAN_POINT('Ctrl Pts',(-3.16435148069425,-1.78359887063561,
253.856285893084));
#14309=CARTESIAN_POINT('Ctrl Pts',(-1.8226963944979,-1.23885301108636,253.921286445967));
#14310=CARTESIAN_POINT('Ctrl Pts',(-0.617266928105228,-0.358596945308037,
253.986286998851));
#14311=CARTESIAN_POINT('Ctrl Pts',(0.31004492907752,0.753553737531672,254.051287551734));
#14312=CARTESIAN_POINT('Ctrl Pts',(1.23735678626026,1.86570442037137,254.116288104617));
#14313=CARTESIAN_POINT('Ctrl Pts',(1.88655103423305,3.20974972027245,254.1812886575));
#14314=CARTESIAN_POINT('Ctrl Pts',(2.18121054041009,4.62748107607727,254.246289210384));
#14315=CARTESIAN_POINT('Ctrl Pts',(2.47587004658713,6.04521243188211,254.311289763267));
#14316=CARTESIAN_POINT('Ctrl Pts',(2.41599481096842,7.53662984359073,254.37629031615));
#14317=CARTESIAN_POINT('Ctrl Pts',(2.0086327915932,8.92617747033215,254.441290869033));
#14318=CARTESIAN_POINT('Ctrl Pts',(1.60127077221798,10.3157250970736,254.506291421917));
#14319=CARTESIAN_POINT('Ctrl Pts',(0.846421969086256,11.6034029388478,254.5712919748));
#14320=CARTESIAN_POINT('Ctrl Pts',(-0.16705980979175,12.6376374894676,254.636292527683));
#14321=CARTESIAN_POINT('Ctrl Pts',(-1.18054158866975,13.6718720400874,254.701293080566));
#14322=CARTESIAN_POINT('Ctrl Pts',(-2.45265634329403,14.4526632995527,254.76629363345));
#14323=CARTESIAN_POINT('Ctrl Pts',(-3.83366250991437,14.8881037542279,254.831294186333));
#14324=CARTESIAN_POINT('Ctrl Pts',(-5.21466867653472,15.3235442089031,254.896294739216));
#14325=CARTESIAN_POINT('Ctrl Pts',(-6.70456625515113,15.4136338587881,254.9612952921));
#14326=CARTESIAN_POINT('Ctrl Pts',(-8.12797830556721,15.1477681849149,255.026295844983));
#14327=CARTESIAN_POINT('Ctrl Pts',(-9.55139035598328,14.8819025110416,255.091296397866));
#14328=CARTESIAN_POINT('Ctrl Pts',(-10.908316878199,14.2600815134102,255.156296950749));
#14329=CARTESIAN_POINT('Ctrl Pts',(-12.0390330528948,13.3555001991571,255.221297503632));
#14330=CARTESIAN_POINT('Ctrl Pts',(-13.1697492275906,12.450918884904,255.286298056516));
#14331=CARTESIAN_POINT('Ctrl Pts',(-14.0742550547665,11.2635772540293,255.351298609399));
#14332=CARTESIAN_POINT('Ctrl Pts',(-14.6460804880105,9.93323816353598,255.416299162282));
#14333=CARTESIAN_POINT('Ctrl Pts',(-15.1197404435826,8.83127886290768,255.470141046887));
#14334=CARTESIAN_POINT('Ctrl Pts',(-15.3651384026615,7.63120471625482,255.523982931492));
#14335=CARTESIAN_POINT('Ctrl Pts',(-15.3662755781924,6.43158183962034,255.577824816097));
#14336=CARTESIAN_POINT('Ctrl Pts',(-15.3665939393721,6.43165874093672,255.944594374291));
#14337=CARTESIAN_POINT('Ctrl Pts',(-15.3657290065113,7.75655071821844,255.885123935126));
#14338=CARTESIAN_POINT('Ctrl Pts',(-15.0645375921236,9.08182296288714,255.825653495962));
#14339=CARTESIAN_POINT('Ctrl Pts',(-14.4901943902724,10.2756876209297,255.766183056797));
#14340=CARTESIAN_POINT('Ctrl Pts',(-13.8624434237493,11.5805689019627,255.701182503914));
#14341=CARTESIAN_POINT('Ctrl Pts',(-12.9083783444587,12.7284673184901,255.636181951031));
#14342=CARTESIAN_POINT('Ctrl Pts',(-11.7403028565014,13.5842629056116,255.571181398147));
#14343=CARTESIAN_POINT('Ctrl Pts',(-10.5722273685442,14.440058492733,255.506180845264));
#14344=CARTESIAN_POINT('Ctrl Pts',(-9.19014147192026,15.0037512504485,255.441180292381));
#14345=CARTESIAN_POINT('Ctrl Pts',(-7.75673151365957,15.2089884884431,255.376179739498));
#14346=CARTESIAN_POINT('Ctrl Pts',(-6.32332155539888,15.4142257264378,255.311179186614));
#14347=CARTESIAN_POINT('Ctrl Pts',(-4.83858753550142,15.2610074447117,255.246178633731));
#14348=CARTESIAN_POINT('Ctrl Pts',(-3.47729858821851,14.767369080426,255.181178080848));
#14349=CARTESIAN_POINT('Ctrl Pts',(-2.11600964093561,14.2737307161403,255.116177527965));
#14350=CARTESIAN_POINT('Ctrl Pts',(-0.878165766267253,13.4396722692951,
255.051176975081));
#14351=CARTESIAN_POINT('Ctrl Pts',(0.0905255226928164,12.3633713731189,
254.986176422198));
#14352=CARTESIAN_POINT('Ctrl Pts',(1.05921681165288,11.2870704769428,254.921175869315));
#14353=CARTESIAN_POINT('Ctrl Pts',(1.75875551490466,9.96852713143572,254.856175316432));
#14354=CARTESIAN_POINT('Ctrl Pts',(2.10679841691598,8.56294804404318,254.791174763548));
#14355=CARTESIAN_POINT('Ctrl Pts',(2.4548413189273,7.15736895665064,254.726174210665));
#14356=CARTESIAN_POINT('Ctrl Pts',(2.45138841969816,5.6647541273726,254.661173657782));
#14357=CARTESIAN_POINT('Ctrl Pts',(2.09684616257126,4.26080034593536,254.596173104898));
#14358=CARTESIAN_POINT('Ctrl Pts',(1.74230390544437,2.85684656449812,254.531172552015));
#14359=CARTESIAN_POINT('Ctrl Pts',(1.03667229041973,1.54155383090168,254.466171999132));
#14360=CARTESIAN_POINT('Ctrl Pts',(0.0630117340679463,0.469746220590651,
254.401171446249));
#14361=CARTESIAN_POINT('Ctrl Pts',(-0.910648822283835,-0.602061389720375,
254.336170893365));
#14362=CARTESIAN_POINT('Ctrl Pts',(-2.15233831996276,-1.43038387674599,
254.271170340482));
#14363=CARTESIAN_POINT('Ctrl Pts',(-3.5158965745936,-1.91771879109464,254.206169787599));
#14364=CARTESIAN_POINT('Ctrl Pts',(-4.87945482922443,-2.4050537054433,254.141169234716));
#14365=CARTESIAN_POINT('Ctrl Pts',(-6.36488184080717,-2.55140104711501,
254.076168681832));
#14366=CARTESIAN_POINT('Ctrl Pts',(-7.79732690288103,-2.33953416283919,
254.011168128949));
#14367=CARTESIAN_POINT('Ctrl Pts',(-9.22977196495487,-2.12766727856337,
253.946167576066));
#14368=CARTESIAN_POINT('Ctrl Pts',(-10.6092350775198,-1.55758616834003,
253.881167023183));
#14369=CARTESIAN_POINT('Ctrl Pts',(-11.7733386226286,-0.696395499103504,
253.816166470299));
#14370=CARTESIAN_POINT('Ctrl Pts',(-12.9374421677373,0.164795170133028,
253.751165917416));
#14371=CARTESIAN_POINT('Ctrl Pts',(-13.8861861453898,1.31709539838274,253.686165364533));
#14372=CARTESIAN_POINT('Ctrl Pts',(-14.5078932039212,2.6248670779529,253.62116481165));
#14373=CARTESIAN_POINT('Ctrl Pts',(-15.0708375808772,3.8090304282859,253.562307999197));
#14374=CARTESIAN_POINT('Ctrl Pts',(-15.3656453212045,5.12066437784316,253.503451186744));
#14375=CARTESIAN_POINT('Ctrl Pts',(-15.3665655929379,6.43189805357513,253.444594374291));
#14376=CARTESIAN_POINT('Origin',(-6.5,6.43177298256785,260.886209595194));
#14377=CARTESIAN_POINT('',(-15.3662080510474,6.43197208529678,250.577824816097));
#14378=CARTESIAN_POINT('',(-15.3658371696729,6.43197914685562,250.944594374291));
#14379=CARTESIAN_POINT('',(-15.366,6.43177298256785,260.886209595194));
#14380=CARTESIAN_POINT('Ctrl Pts',(-15.3662080510474,6.43197208529678,250.577824816097));
#14381=CARTESIAN_POINT('Ctrl Pts',(-15.365069838388,5.25528049615197,250.63063632896));
#14382=CARTESIAN_POINT('Ctrl Pts',(-15.1292211412892,4.07814608026942,250.683447841824));
#14383=CARTESIAN_POINT('Ctrl Pts',(-14.6730366414472,2.99369826140245,250.736259354687));
#14384=CARTESIAN_POINT('Ctrl Pts',(-14.1115635250993,1.65895695259718,250.801259907571));
#14385=CARTESIAN_POINT('Ctrl Pts',(-13.2163091438145,0.464624280106945,
250.866260460454));
#14386=CARTESIAN_POINT('Ctrl Pts',(-12.0926545495139,-0.448713978436843,
250.931261013337));
#14387=CARTESIAN_POINT('Ctrl Pts',(-10.9689999552133,-1.36205223698062,
250.996261566221));
#14388=CARTESIAN_POINT('Ctrl Pts',(-9.61694514789703,-1.99439608157795,
251.061262119104));
#14389=CARTESIAN_POINT('Ctrl Pts',(-8.19564149373379,-2.27131185302248,
251.126262671987));
#14390=CARTESIAN_POINT('Ctrl Pts',(-6.77433783957052,-2.54822762446701,
251.19126322487));
#14391=CARTESIAN_POINT('Ctrl Pts',(-5.2837853385603,-2.46971532275872,251.256263777754));
#14392=CARTESIAN_POINT('Ctrl Pts',(-3.89943802229893,-2.0450166886986,251.321264330637));
#14393=CARTESIAN_POINT('Ctrl Pts',(-2.51509070603756,-1.62031805463848,
251.38626488352));
#14394=CARTESIAN_POINT('Ctrl Pts',(-1.23694857452505,-0.849433088226517,
251.451265436403));
#14395=CARTESIAN_POINT('Ctrl Pts',(-0.215462678478693,0.1768967739479,251.516265989287));
#14396=CARTESIAN_POINT('Ctrl Pts',(0.806023217567654,1.20322663612231,251.58126654217));
#14397=CARTESIAN_POINT('Ctrl Pts',(1.57085287814786,2.4850013940592,251.646267095053));
#14398=CARTESIAN_POINT('Ctrl Pts',(1.98899764117726,3.87134239791202,251.711267647936));
#14399=CARTESIAN_POINT('Ctrl Pts',(2.40714240420666,5.25768340176484,251.77626820082));
#14400=CARTESIAN_POINT('Ctrl Pts',(2.47860226968529,6.74859065153357,251.841268753703));
#14401=CARTESIAN_POINT('Ctrl Pts',(2.19496564426971,8.16856835788513,251.906269306586));
#14402=CARTESIAN_POINT('Ctrl Pts',(1.91132901885414,9.58854606423668,251.971269859469));
#14403=CARTESIAN_POINT('Ctrl Pts',(1.27259590254435,10.937594227171,252.036270412353));
#14404=CARTESIAN_POINT('Ctrl Pts',(0.353952040421027,12.0569153948417,252.101270965236));
#14405=CARTESIAN_POINT('Ctrl Pts',(-0.564691821702289,13.1762365625124,
252.166271518119));
#14406=CARTESIAN_POINT('Ctrl Pts',(-1.76324642963914,14.0658307349195,252.231272071002));
#14407=CARTESIAN_POINT('Ctrl Pts',(-3.10062903863032,14.6209831274933,252.296272623886));
#14408=CARTESIAN_POINT('Ctrl Pts',(-4.43801164762152,15.1761355200672,252.361273176769));
#14409=CARTESIAN_POINT('Ctrl Pts',(-5.91422225766704,15.3968461328078,252.426273729652));
#14410=CARTESIAN_POINT('Ctrl Pts',(-7.35549503170888,15.2571349570976,252.491274282535));
#14411=CARTESIAN_POINT('Ctrl Pts',(-8.7967678057507,15.1174237813874,252.556274835419));
#14412=CARTESIAN_POINT('Ctrl Pts',(-10.2031027437888,14.6172908172262,252.621275388302));
#14413=CARTESIAN_POINT('Ctrl Pts',(-11.4089591255296,13.8156070838078,252.686275941185));
#14414=CARTESIAN_POINT('Ctrl Pts',(-12.6148155072703,13.0139233503894,252.751276494069));
#14415=CARTESIAN_POINT('Ctrl Pts',(-13.6201933327137,11.9106888477137,252.816277046952));
#14416=CARTESIAN_POINT('Ctrl Pts',(-14.3067488383011,10.6357661208161,252.881277599835));
#14417=CARTESIAN_POINT('Ctrl Pts',(-14.9933043438886,9.36084339391843,252.946278152718));
#14418=CARTESIAN_POINT('Ctrl Pts',(-15.3610375296202,7.91423244279888,253.011278705602));
#14419=CARTESIAN_POINT('Ctrl Pts',(-15.3666622516369,6.46621490688475,253.076279258485));
#14420=CARTESIAN_POINT('Ctrl Pts',(-15.3667068324471,6.45473810950495,253.076794444356));
#14421=CARTESIAN_POINT('Ctrl Pts',(-15.3667286658208,6.44326122376433,253.077309630226));
#14422=CARTESIAN_POINT('Ctrl Pts',(-15.3667277726507,6.43178433461072,253.077824816097));
#14423=CARTESIAN_POINT('Ctrl Pts',(-15.3665655929379,6.43189805357513,253.444594374291));
#14424=CARTESIAN_POINT('Ctrl Pts',(-15.3666616550659,6.5687705584125,253.43845063386));
#14425=CARTESIAN_POINT('Ctrl Pts',(-15.363555481387,6.70563870181459,253.43230689343));
#14426=CARTESIAN_POINT('Ctrl Pts',(-15.3572177832327,6.84235704507857,253.426163153));
#14427=CARTESIAN_POINT('Ctrl Pts',(-15.2901651646025,8.28883220174352,253.361162600116));
#14428=CARTESIAN_POINT('Ctrl Pts',(-14.8613897879318,9.71853938418283,253.296162047233));
#14429=CARTESIAN_POINT('Ctrl Pts',(-14.1213631182881,10.963186708018,253.23116149435));
#14430=CARTESIAN_POINT('Ctrl Pts',(-13.3813364486445,12.2078340318531,253.166160941467));
#14431=CARTESIAN_POINT('Ctrl Pts',(-12.3300584860279,13.2674214970841,253.101160388583));
#14432=CARTESIAN_POINT('Ctrl Pts',(-11.0912759329153,14.0172242835672,253.0361598357));
#14433=CARTESIAN_POINT('Ctrl Pts',(-9.85249337980274,14.7670270700503,252.971159282817));
#14434=CARTESIAN_POINT('Ctrl Pts',(-8.4262062361942,15.2070451777856,252.906158729934));
#14435=CARTESIAN_POINT('Ctrl Pts',(-6.98030381118131,15.2854837515599,252.84115817705));
#14436=CARTESIAN_POINT('Ctrl Pts',(-5.53440138616842,15.3639223253342,252.776157624167));
#14437=CARTESIAN_POINT('Ctrl Pts',(-4.06888367975118,15.0807813651476,252.711157071284));
#14438=CARTESIAN_POINT('Ctrl Pts',(-2.756257859434,14.4693896017499,252.646156518401));
#14439=CARTESIAN_POINT('Ctrl Pts',(-1.44363203911683,13.8579978383522,252.581155965517));
#14440=CARTESIAN_POINT('Ctrl Pts',(-0.283898104899725,12.9183552717433,
252.516155412634));
#14441=CARTESIAN_POINT('Ctrl Pts',(0.586430808524681,11.7610679197985,252.451154859751));
#14442=CARTESIAN_POINT('Ctrl Pts',(1.45675972194909,10.6037805678537,252.386154306867));
#14443=CARTESIAN_POINT('Ctrl Pts',(2.03768361458079,9.22884843057297,252.321153753984));
#14444=CARTESIAN_POINT('Ctrl Pts',(2.2608215075925,7.79811578146756,252.256153201101));
#14445=CARTESIAN_POINT('Ctrl Pts',(2.48395940060421,6.36738313236216,252.191152648218));
#14446=CARTESIAN_POINT('Ctrl Pts',(2.34931129399593,4.88084997143212,252.126152095335));
#14447=CARTESIAN_POINT('Ctrl Pts',(1.87272671546639,3.5134972107951,252.061151542451));
#14448=CARTESIAN_POINT('Ctrl Pts',(1.39614213693684,2.14614445015806,251.996150989568));
#14449=CARTESIAN_POINT('Ctrl Pts',(0.577621086486011,0.897972089814032,
251.931150436685));
#14450=CARTESIAN_POINT('Ctrl Pts',(-0.486487720795355,-0.0840965833347244,
251.866149883801));
#14451=CARTESIAN_POINT('Ctrl Pts',(-1.55059652807671,-1.06616525648347,
251.801149330918));
#14452=CARTESIAN_POINT('Ctrl Pts',(-2.86029309218863,-1.78213024243697,
251.736148778035));
#14453=CARTESIAN_POINT('Ctrl Pts',(-4.26141206693571,-2.14771477591397,
251.671148225152));
#14454=CARTESIAN_POINT('Ctrl Pts',(-5.6625310416828,-2.51329930939097,251.606147672268));
#14455=CARTESIAN_POINT('Ctrl Pts',(-7.15507242706507,-2.52850339039149,
251.541147119385));
#14456=CARTESIAN_POINT('Ctrl Pts',(-8.56334807844394,-2.19153733535427,
251.476146566502));
#14457=CARTESIAN_POINT('Ctrl Pts',(-9.9716237298228,-1.85457128031705,251.411146013619));
#14458=CARTESIAN_POINT('Ctrl Pts',(-11.2956336471983,-1.1654350892421,251.346145460735));
#14459=CARTESIAN_POINT('Ctrl Pts',(-12.379527649031,-0.205247490225679,
251.281144907852));
#14460=CARTESIAN_POINT('Ctrl Pts',(-13.4634216508637,0.754940108790739,
251.216144354969));
#14461=CARTESIAN_POINT('Ctrl Pts',(-14.3071997371537,1.98617911574862,251.151143802085));
#14462=CARTESIAN_POINT('Ctrl Pts',(-14.8115401685383,3.34353948123183,251.086143249202));
#14463=CARTESIAN_POINT('Ctrl Pts',(-15.1776335706624,4.32882767782522,251.038960290898));
#14464=CARTESIAN_POINT('Ctrl Pts',(-15.3648739637955,5.38057044757596,250.991777332594));
#14465=CARTESIAN_POINT('Ctrl Pts',(-15.3658371696729,6.43197914685562,250.944594374291));
#14466=CARTESIAN_POINT('Origin',(-6.5,6.43177298256785,260.886209595194));
#14467=CARTESIAN_POINT('',(-15.3655097454245,6.43192356724116,248.077824816097));
#14468=CARTESIAN_POINT('',(-15.3653398059476,6.43183049307641,248.444594374291));
#14469=CARTESIAN_POINT('',(-15.366,6.43177298256785,260.886209595194));
#14470=CARTESIAN_POINT('Ctrl Pts',(-15.3655097454245,6.43192356724116,248.077824816097));
#14471=CARTESIAN_POINT('Ctrl Pts',(-15.3649315115624,5.51512897749327,248.118962474811));
#14472=CARTESIAN_POINT('Ctrl Pts',(-15.2233361525865,4.59815980571514,248.160100133526));
#14473=CARTESIAN_POINT('Ctrl Pts',(-14.94362213897,3.72545982623404,248.20123779224));
#14474=CARTESIAN_POINT('Ctrl Pts',(-14.5016532447144,2.34652911067504,248.266238345123));
#14475=CARTESIAN_POINT('Ctrl Pts',(-13.7148525584771,1.07812238587667,248.331238898007));
#14476=CARTESIAN_POINT('Ctrl Pts',(-12.6758349667039,0.0695447410792356,
248.39623945089));
#14477=CARTESIAN_POINT('Ctrl Pts',(-11.6368173749308,-0.939032903718183,
248.461240003773));
#14478=CARTESIAN_POINT('Ctrl Pts',(-10.3455828776218,-1.68778146851468,
248.526240556656));
#14479=CARTESIAN_POINT('Ctrl Pts',(-8.95412363807302,-2.08856520903101,
248.59124110954));
#14480=CARTESIAN_POINT('Ctrl Pts',(-7.56266439852423,-2.48934894954734,
248.656241662423));
#14481=CARTESIAN_POINT('Ctrl Pts',(-6.07098041673563,-2.54216786578351,
248.721242215306));
#14482=CARTESIAN_POINT('Ctrl Pts',(-4.6546589114767,-2.24080460416003,248.786242768189));
#14483=CARTESIAN_POINT('Ctrl Pts',(-3.23833740621773,-1.93944134253654,
248.851243321073));
#14484=CARTESIAN_POINT('Ctrl Pts',(-1.89737837748844,-1.28389590305338,
248.916243873956));
#14485=CARTESIAN_POINT('Ctrl Pts',(-0.789627099316419,-0.351333021761874,
248.981244426839));
#14486=CARTESIAN_POINT('Ctrl Pts',(0.318124178855573,0.581229859529608,
249.046244979723));
#14487=CARTESIAN_POINT('Ctrl Pts',(1.19266770647031,1.79081018262943,249.111245532606));
#14488=CARTESIAN_POINT('Ctrl Pts',(1.7310603214858,3.13502735775253,249.176246085489));
#14489=CARTESIAN_POINT('Ctrl Pts',(2.26945293650129,4.47924453287563,249.241246638372));
#14490=CARTESIAN_POINT('Ctrl Pts',(2.47169463891752,5.95809856002202,249.306247191256));
#14491=CARTESIAN_POINT('Ctrl Pts',(2.31397940911453,7.39751244355334,249.371247744139));
#14492=CARTESIAN_POINT('Ctrl Pts',(2.15626417931155,8.83692632708468,249.436248297022));
#14493=CARTESIAN_POINT('Ctrl Pts',(1.63859201728934,10.236900067001,249.501248849905));
#14494=CARTESIAN_POINT('Ctrl Pts',(0.821898494138215,11.4326417243236,249.566249402789));
#14495=CARTESIAN_POINT('Ctrl Pts',(0.00520497098708925,12.6283833816463,
249.631249955672));
#14496=CARTESIAN_POINT('Ctrl Pts',(-1.11050991329295,13.6198929563754,249.696250508555));
#14497=CARTESIAN_POINT('Ctrl Pts',(-2.3939145387706,14.290459126946,249.761251061438));
#14498=CARTESIAN_POINT('Ctrl Pts',(-3.67731916424824,14.9610252975167,249.826251614322));
#14499=CARTESIAN_POINT('Ctrl Pts',(-5.12841353092349,15.3106480639289,249.891252167205));
#14500=CARTESIAN_POINT('Ctrl Pts',(-6.5763882532227,15.2981730731075,249.956252720088));
#14501=CARTESIAN_POINT('Ctrl Pts',(-8.02436297552191,15.2856980822862,250.021253272971));
#14502=CARTESIAN_POINT('Ctrl Pts',(-9.46921805344508,14.9111253342314,250.086253825855));
#14503=CARTESIAN_POINT('Ctrl Pts',(-10.7408785326919,14.2185460627152,250.151254378738));
#14504=CARTESIAN_POINT('Ctrl Pts',(-12.0125390119386,13.5259667911989,250.216254931621));
#14505=CARTESIAN_POINT('Ctrl Pts',(-13.111004892509,12.5153809962213,250.281255484505));
#14506=CARTESIAN_POINT('Ctrl Pts',(-13.9069749473838,11.3057454752666,250.346256037388));
#14507=CARTESIAN_POINT('Ctrl Pts',(-14.7029450022585,10.0961099543118,250.411256590271));
#14508=CARTESIAN_POINT('Ctrl Pts',(-15.1964192314376,8.68742470738009,250.476257143154));
#14509=CARTESIAN_POINT('Ctrl Pts',(-15.3293104203217,7.24550711135407,250.541257696038));
#14510=CARTESIAN_POINT('Ctrl Pts',(-15.3542304548097,6.97511569922655,250.553446736057));
#14511=CARTESIAN_POINT('Ctrl Pts',(-15.366470753608,6.70355568692715,250.565635776077));
#14512=CARTESIAN_POINT('Ctrl Pts',(-15.3662080510474,6.43197208529678,250.577824816097));
#14513=CARTESIAN_POINT('Ctrl Pts',(-15.3658371696729,6.43197914685562,250.944594374291));
#14514=CARTESIAN_POINT('Ctrl Pts',(-15.3662009029452,6.82902025267945,250.926776779711));
#14515=CARTESIAN_POINT('Ctrl Pts',(-15.3400010025069,7.22601371914519,250.908959185132));
#14516=CARTESIAN_POINT('Ctrl Pts',(-15.2868376708262,7.61936292802496,250.891141590552));
#14517=CARTESIAN_POINT('Ctrl Pts',(-15.0928919652502,9.05434428532636,250.826141037669));
#14518=CARTESIAN_POINT('Ctrl Pts',(-14.5400977776192,10.4408252759206,250.761140484786));
#14519=CARTESIAN_POINT('Ctrl Pts',(-13.6935249184878,11.6156022022756,250.696139931903));
#14520=CARTESIAN_POINT('Ctrl Pts',(-12.8469520593564,12.7903791286305,250.631139379019));
#14521=CARTESIAN_POINT('Ctrl Pts',(-11.7066005287246,13.7534519907462,250.566138826136));
#14522=CARTESIAN_POINT('Ctrl Pts',(-10.4067019442981,14.391456773424,250.501138273253));
#14523=CARTESIAN_POINT('Ctrl Pts',(-9.10680335987154,15.0294615561018,250.43613772037));
#14524=CARTESIAN_POINT('Ctrl Pts',(-7.64735772165025,15.3423982593419,250.371137167486));
#14525=CARTESIAN_POINT('Ctrl Pts',(-6.20015744952368,15.2934308735567,250.306136614603));
#14526=CARTESIAN_POINT('Ctrl Pts',(-4.75295717739709,15.2444634877715,250.24113606172));
#14527=CARTESIAN_POINT('Ctrl Pts',(-3.3180022713652,14.833592012961,250.176135508837));
#14528=CARTESIAN_POINT('Ctrl Pts',(-2.06420232921192,14.1091804327317,250.111134955953));
#14529=CARTESIAN_POINT('Ctrl Pts',(-0.810402387058642,13.3847688525024,
250.04613440307));
#14530=CARTESIAN_POINT('Ctrl Pts',(0.262242591216055,12.3468171668541,249.981133850187));
#14531=CARTESIAN_POINT('Ctrl Pts',(1.02747077600075,11.1175034323969,249.916133297303));
#14532=CARTESIAN_POINT('Ctrl Pts',(1.79269896078545,9.88818969793975,249.85113274442));
#14533=CARTESIAN_POINT('Ctrl Pts',(2.25051035208017,8.46751391467371,249.786132191537));
#14534=CARTESIAN_POINT('Ctrl Pts',(2.34701563417244,7.0227048743358,249.721131638654));
#14535=CARTESIAN_POINT('Ctrl Pts',(2.44352091626472,5.57789583399789,249.65613108577));
#14536=CARTESIAN_POINT('Ctrl Pts',(2.17872008915453,4.10895353658814,249.591130532887));
#14537=CARTESIAN_POINT('Ctrl Pts',(1.58378305303297,2.78878826073631,249.526129980004));
#14538=CARTESIAN_POINT('Ctrl Pts',(0.988846016911408,1.46862298488449,249.461129427121));
#14539=CARTESIAN_POINT('Ctrl Pts',(0.0637727717784695,0.29723473059058,
249.396128874237));
#14540=CARTESIAN_POINT('Ctrl Pts',(-1.08254563004082,-0.587491528861413,
249.331128321354));
#14541=CARTESIAN_POINT('Ctrl Pts',(-2.22886403186013,-1.47221778831342,
249.266127768471));
#14542=CARTESIAN_POINT('Ctrl Pts',(-3.59642759036579,-2.0702820529235,249.201127215588));
#14543=CARTESIAN_POINT('Ctrl Pts',(-5.02425939287671,-2.31128573806799,
249.136126662704));
#14544=CARTESIAN_POINT('Ctrl Pts',(-6.45209119538764,-2.55228942321248,
249.071126109821));
#14545=CARTESIAN_POINT('Ctrl Pts',(-7.94019124190381,-2.43623252889138,
249.006125556938));
#14546=CARTESIAN_POINT('Ctrl Pts',(-9.31339418105008,-1.97677619752506,
248.941125004055));
#14547=CARTESIAN_POINT('Ctrl Pts',(-10.6865971201963,-1.51731986615874,
248.876124451171));
#14548=CARTESIAN_POINT('Ctrl Pts',(-11.9449029519726,-0.714464097747203,
248.811123898288));
#14549=CARTESIAN_POINT('Ctrl Pts',(-12.9401955711036,0.33728636449107,248.746123345405));
#14550=CARTESIAN_POINT('Ctrl Pts',(-13.9354881902347,1.38903682672936,248.681122792522));
#14551=CARTESIAN_POINT('Ctrl Pts',(-14.6677675967203,2.68968198279439,248.616122239638));
#14552=CARTESIAN_POINT('Ctrl Pts',(-15.0508366428241,4.08612193439743,248.551121686755));
#14553=CARTESIAN_POINT('Ctrl Pts',(-15.2601031498491,4.84898208693241,248.5156125826));
#14554=CARTESIAN_POINT('Ctrl Pts',(-15.3651541248176,5.64043046799048,248.480103478445));
#14555=CARTESIAN_POINT('Ctrl Pts',(-15.3653398059476,6.43183049307641,248.444594374291));
#14556=CARTESIAN_POINT('Origin',(-6.5,6.43177298256785,260.886209595194));
#14557=CARTESIAN_POINT('',(-15.3653307732302,6.43170986456378,245.577824816097));
#14558=CARTESIAN_POINT('',(-15.3655110343894,6.43162198763813,245.944594374291));
#14559=CARTESIAN_POINT('',(-15.366,6.43177298256785,260.886209595194));
#14560=CARTESIAN_POINT('Ctrl Pts',(-15.3653307732302,6.43170986456378,245.577824816097));
#14561=CARTESIAN_POINT('Ctrl Pts',(-15.365491947844,5.77504272427858,245.607288620662));
#14562=CARTESIAN_POINT('Ctrl Pts',(-15.293456027428,5.1184079823648,245.636752425228));
#14563=CARTESIAN_POINT('Ctrl Pts',(-15.1488419680877,4.47816742424782,245.666216229793));
#14564=CARTESIAN_POINT('Ctrl Pts',(-14.8298066652648,3.06572287169104,245.731216782676));
#14565=CARTESIAN_POINT('Ctrl Pts',(-14.1575375418244,1.73306791231306,245.796217335559));
#14566=CARTESIAN_POINT('Ctrl Pts',(-13.2111975505435,0.637061396213097,
245.861217888443));
#14567=CARTESIAN_POINT('Ctrl Pts',(-12.2648575592627,-0.458945119886869,
245.926218441326));
#14568=CARTESIAN_POINT('Ctrl Pts',(-11.0444467001413,-1.31830319270885,
245.991218994209));
#14569=CARTESIAN_POINT('Ctrl Pts',(-9.69360663159018,-1.83985231435453,
246.056219547092));
#14570=CARTESIAN_POINT('Ctrl Pts',(-8.34276656303907,-2.36140143600022,
246.121220099976));
#14571=CARTESIAN_POINT('Ctrl Pts',(-6.86149728505829,-2.54514160646962,
246.186220652859));
#14572=CARTESIAN_POINT('Ctrl Pts',(-5.42416640013887,-2.36944666273369,
246.251221205742));
#14573=CARTESIAN_POINT('Ctrl Pts',(-3.98683551521946,-2.19375171899776,
246.316221758626));
#14574=CARTESIAN_POINT('Ctrl Pts',(-2.59344302336147,-1.65862166105649,
246.381222311509));
#14575=CARTESIAN_POINT('Ctrl Pts',(-1.40800326731247,-0.827046055025128,
246.446222864392));
#14576=CARTESIAN_POINT('Ctrl Pts',(-0.222563511263459,0.00452955100623695,
246.511223417275));
#14577=CARTESIAN_POINT('Ctrl Pts',(0.754923508976573,1.13255070512771,246.576223970159));
#14578=CARTESIAN_POINT('Ctrl Pts',(1.40939574037707,2.4242367681619,246.641224523042));
#14579=CARTESIAN_POINT('Ctrl Pts',(2.06386797177757,3.71592283119607,246.706225075925));
#14580=CARTESIAN_POINT('Ctrl Pts',(2.39532541433854,5.17127380314298,246.771225628808));
#14581=CARTESIAN_POINT('Ctrl Pts',(2.36475258440544,6.6189794563542,246.836226181692));
#14582=CARTESIAN_POINT('Ctrl Pts',(2.33417975447233,8.06668510956546,246.901226734575));
#14583=CARTESIAN_POINT('Ctrl Pts',(1.94157665204511,9.50674544404105,246.966227287458));
#14584=CARTESIAN_POINT('Ctrl Pts',(1.23315659414109,10.7696498045689,247.031227840341));
#14585=CARTESIAN_POINT('Ctrl Pts',(0.524736536237075,12.0325541650966,247.096228393225));
#14586=CARTESIAN_POINT('Ctrl Pts',(-0.499500477143713,13.1183025516767,
247.161228946108));
#14587=CARTESIAN_POINT('Ctrl Pts',(-1.71899062328603,13.8990907662661,247.226229498991));
#14588=CARTESIAN_POINT('Ctrl Pts',(-2.93848076942834,14.6798789808555,247.291230051874));
#14589=CARTESIAN_POINT('Ctrl Pts',(-4.35322404833216,15.1557070234544,247.356230604758));
#14590=CARTESIAN_POINT('Ctrl Pts',(-5.79669004762257,15.2705648051858,247.421231157641));
#14591=CARTESIAN_POINT('Ctrl Pts',(-7.240156046913,15.3854225869173,247.486231710524));
#14592=CARTESIAN_POINT('Ctrl Pts',(-8.71234476659003,15.1393101077814,247.551232263407));
#14593=CARTESIAN_POINT('Ctrl Pts',(-10.0399637617057,14.5611974579483,247.616232816291));
#14594=CARTESIAN_POINT('Ctrl Pts',(-11.3675827568214,13.9830848081152,247.681233369174));
#14595=CARTESIAN_POINT('Ctrl Pts',(-12.5506320273757,13.072971987585,247.746233922057));
#14596=CARTESIAN_POINT('Ctrl Pts',(-13.4498539859601,11.9379890418828,247.811234474941));
#14597=CARTESIAN_POINT('Ctrl Pts',(-14.3490759445444,10.8030060961806,247.876235027824));
#14598=CARTESIAN_POINT('Ctrl Pts',(-14.9644705911588,9.44315302530647,247.941235580707));
#14599=CARTESIAN_POINT('Ctrl Pts',(-15.223599363329,8.01849913670959,248.00623613359));
#14600=CARTESIAN_POINT('Ctrl Pts',(-15.3187302844077,7.49548258588289,248.030099027759));
#14601=CARTESIAN_POINT('Ctrl Pts',(-15.3658451639653,6.96373244877257,248.053961921928));
#14602=CARTESIAN_POINT('Ctrl Pts',(-15.3655097454245,6.43192356724116,248.077824816097));
#14603=CARTESIAN_POINT('Ctrl Pts',(-15.3653398059476,6.43183049307641,248.444594374291));
#14604=CARTESIAN_POINT('Ctrl Pts',(-15.3654940200753,7.08911357072862,248.415102925562));
#14605=CARTESIAN_POINT('Ctrl Pts',(-15.2933138879128,7.74636329323055,248.385611476834));
#14606=CARTESIAN_POINT('Ctrl Pts',(-15.1484271692047,8.38717412578271,248.356120028105));
#14607=CARTESIAN_POINT('Ctrl Pts',(-14.8290899637598,9.79955161842378,248.291119475222));
#14608=CARTESIAN_POINT('Ctrl Pts',(-14.1565568671482,11.1320718565649,248.226118922339));
#14609=CARTESIAN_POINT('Ctrl Pts',(-13.2099922449493,12.2278829025747,248.161118369455));
#14610=CARTESIAN_POINT('Ctrl Pts',(-12.2634276227504,13.3236939485845,248.096117816572));
#14611=CARTESIAN_POINT('Ctrl Pts',(-11.0428314749641,14.182795802463,248.031117263689));
#14612=CARTESIAN_POINT('Ctrl Pts',(-9.69188107233505,14.7040629528314,247.966116710806));
#14613=CARTESIAN_POINT('Ctrl Pts',(-8.34093066970603,15.2253301031998,247.901116157922));
#14614=CARTESIAN_POINT('Ctrl Pts',(-6.8596260122343,15.4087625500582,247.836115605039));
#14615=CARTESIAN_POINT('Ctrl Pts',(-5.42233256080435,15.2327683252499,247.771115052156));
#14616=CARTESIAN_POINT('Ctrl Pts',(-3.98503910937443,15.0567741004416,247.706114499273));
#14617=CARTESIAN_POINT('Ctrl Pts',(-2.5917568639863,14.5213532039666,247.641113946389));
#14618=CARTESIAN_POINT('Ctrl Pts',(-1.40649010340869,13.6895304232192,247.576113393506));
#14619=CARTESIAN_POINT('Ctrl Pts',(-0.221223342831083,12.8577076424717,
247.511112840623));
#14620=CARTESIAN_POINT('Ctrl Pts',(0.756027932935998,11.7294829774518,247.44611228774));
#14621=CARTESIAN_POINT('Ctrl Pts',(1.41023075834464,10.4376605841909,247.381111734856));
#14622=CARTESIAN_POINT('Ctrl Pts',(2.06443358375329,9.14583819092992,247.316111181973));
#14623=CARTESIAN_POINT('Ctrl Pts',(2.3955879588035,7.69041806942788,247.25111062909));
#14624=CARTESIAN_POINT('Ctrl Pts',(2.36471345584747,6.24271879173646,247.186110076207));
#14625=CARTESIAN_POINT('Ctrl Pts',(2.33383895289144,4.79501951404503,247.121109523323));
#14626=CARTESIAN_POINT('Ctrl Pts',(1.94093557192917,3.35504108016422,247.05610897044));
#14627=CARTESIAN_POINT('Ctrl Pts',(1.23225226447099,2.09228441387053,246.991108417557));
#14628=CARTESIAN_POINT('Ctrl Pts',(0.523568957012813,0.829527747576842,
246.926107864673));
#14629=CARTESIAN_POINT('Ctrl Pts',(-0.500894276941281,-0.256007151129717,
246.86110731179));
#14630=CARTESIAN_POINT('Ctrl Pts',(-1.7205471282046,-1.03654117677531,246.796106758907));
#14631=CARTESIAN_POINT('Ctrl Pts',(-2.94019997946792,-1.81707520242089,
246.731106206024));
#14632=CARTESIAN_POINT('Ctrl Pts',(-4.35504244804047,-2.29260835500551,
246.66610565314));
#14633=CARTESIAN_POINT('Ctrl Pts',(-5.79853236018863,-2.40716526386096,
246.601105100257));
#14634=CARTESIAN_POINT('Ctrl Pts',(-7.24202227233679,-2.5217221727164,246.536104547374));
#14635=CARTESIAN_POINT('Ctrl Pts',(-8.71415962806057,-2.27530283784268,
246.471103994491));
#14636=CARTESIAN_POINT('Ctrl Pts',(-10.0416581120634,-1.69691348952389,
246.406103441607));
#14637=CARTESIAN_POINT('Ctrl Pts',(-11.3691565960662,-1.11852414120512,
246.341102888724));
#14638=CARTESIAN_POINT('Ctrl Pts',(-12.552016208348,-0.208164779441313,
246.276102335841));
#14639=CARTESIAN_POINT('Ctrl Pts',(-13.4510015518931,0.927005588855917,
246.211101782958));
#14640=CARTESIAN_POINT('Ctrl Pts',(-14.3499868954382,2.06217595715318,246.146101230074));
#14641=CARTESIAN_POINT('Ctrl Pts',(-14.9650979702466,3.42215733198388,246.081100677191));
#14642=CARTESIAN_POINT('Ctrl Pts',(-15.2239298637372,4.84686516798998,246.016100124308));
#14643=CARTESIAN_POINT('Ctrl Pts',(-15.3188417162853,5.36929560819389,245.992264874302));
#14644=CARTESIAN_POINT('Ctrl Pts',(-15.365846922726,5.90042941315193,245.968429624296));
#14645=CARTESIAN_POINT('Ctrl Pts',(-15.3655110343894,6.43162198763813,245.944594374291));
#14646=CARTESIAN_POINT('Origin',(-6.5,6.43177298256785,263.507698758713));
#14647=CARTESIAN_POINT('',(-13.9450882934309,6.43189944074375,247.257698758713));
#14648=CARTESIAN_POINT('',(-13.9450893758793,6.43164617986677,246.764720431675));
#14649=CARTESIAN_POINT('',(-13.9455,6.43177298256789,263.507698758713));
#14650=CARTESIAN_POINT('',(-13.5606802741685,4.06871967504022,244.886209595194));
#14651=CARTESIAN_POINT('Ctrl Pts',(-13.9450882934309,6.43189944074375,247.257698758713));
#14652=CARTESIAN_POINT('Ctrl Pts',(-13.9453699716111,6.8785025342968,247.233835864544));
#14653=CARTESIAN_POINT('Ctrl Pts',(-13.7980287498298,8.54143185980366,247.144972417492));
#14654=CARTESIAN_POINT('Ctrl Pts',(-12.5747094635392,11.2446313388274,246.991108417557));
#14655=CARTESIAN_POINT('Ctrl Pts',(-9.59420190300037,13.5375182117999,246.796106758907));
#14656=CARTESIAN_POINT('Ctrl Pts',(-5.88525273346894,14.1575601010644,246.601105100257));
#14657=CARTESIAN_POINT('Ctrl Pts',(-2.3210283651816,12.9587857864344,246.406103441607));
#14658=CARTESIAN_POINT('Ctrl Pts',(0.259376558051009,10.2234125812861,246.211101782958));
#14659=CARTESIAN_POINT('Ctrl Pts',(1.24847865565592,6.59540585209445,246.016100124308));
#14660=CARTESIAN_POINT('Ctrl Pts',(0.413423482436507,2.92887675386613,245.821098465658));
#14661=CARTESIAN_POINT('Ctrl Pts',(-2.04920214666245,0.0870039240630693,
245.626096807008));
#14662=CARTESIAN_POINT('Ctrl Pts',(-5.55963654711201,-1.26117254099502,
245.431095148358));
#14663=CARTESIAN_POINT('Ctrl Pts',(-9.29146276272433,-0.798267925870965,
245.236093489709));
#14664=CARTESIAN_POINT('Ctrl Pts',(-12.1552397329513,1.21827415889713,245.054464971987));
#14665=CARTESIAN_POINT('Ctrl Pts',(-13.2531691625695,3.15293886147087,244.937837007149));
#14666=CARTESIAN_POINT('Ctrl Pts',(-13.5606802741685,4.06871967504022,244.886209595194));
#14667=CARTESIAN_POINT('',(-6.56569596473014,-1.01343717499105,244.886209595194));
#14668=CARTESIAN_POINT('Origin',(-6.5,6.43177298256785,244.886209595194));
#14669=CARTESIAN_POINT('Ctrl Pts',(-13.9450893758793,6.43164617986677,246.764720431674));
#14670=CARTESIAN_POINT('Ctrl Pts',(-13.9446022147054,7.20207006749424,246.723555128797));
#14671=CARTESIAN_POINT('Ctrl Pts',(-13.6375150380194,9.18938303346644,246.617389273036));
#14672=CARTESIAN_POINT('Ctrl Pts',(-11.8969968350143,11.9939777077968,246.446222864392));
#14673=CARTESIAN_POINT('Ctrl Pts',(-8.64354351795149,13.8796529333669,246.251221205742));
#14674=CARTESIAN_POINT('Ctrl Pts',(-4.88544464111068,14.0119423198044,246.056219547092));
#14675=CARTESIAN_POINT('Ctrl Pts',(-1.50746712882826,12.3596870112171,245.861217888443));
#14676=CARTESIAN_POINT('Ctrl Pts',(0.695205395144706,9.31189841214496,245.666216229793));
#14677=CARTESIAN_POINT('Ctrl Pts',(1.20387608653361,5.58602334650667,245.471214571143));
#14678=CARTESIAN_POINT('Ctrl Pts',(-0.100899992062858,2.05939046574996,
245.276212912493));
#14679=CARTESIAN_POINT('Ctrl Pts',(-2.91261395215861,-0.438036016167426,
245.081211253844));
#14680=CARTESIAN_POINT('Ctrl Pts',(-5.34941510741743,-1.02416954420736,
244.951210148077));
#14681=CARTESIAN_POINT('Ctrl Pts',(-6.56569596473014,-1.01343717499105,
244.886209595194));
#14682=CARTESIAN_POINT('Origin',(-6.5,6.43177298256785,263.507698758713));
#14683=CARTESIAN_POINT('',(-13.9456747173555,6.43194018529407,249.757698758713));
#14684=CARTESIAN_POINT('',(-13.9449455814553,6.43182127881114,249.264720431674));
#14685=CARTESIAN_POINT('',(-13.9455,6.43177298256789,263.507698758713));
#14686=CARTESIAN_POINT('Ctrl Pts',(-13.9456747173555,6.43194018529407,249.757698758713));
#14687=CARTESIAN_POINT('Ctrl Pts',(-13.9458953300235,6.66001098452012,249.745509718693));
#14688=CARTESIAN_POINT('Ctrl Pts',(-13.8808003634927,8.10419059181383,249.66832012579));
#14689=CARTESIAN_POINT('Ctrl Pts',(-12.9742685135307,10.6920016007892,249.526129980004));
#14690=CARTESIAN_POINT('Ctrl Pts',(-10.2068555718026,13.2380144148563,249.331128321354));
#14691=CARTESIAN_POINT('Ctrl Pts',(-6.56676923658599,14.1816918552946,249.136126662704));
#14692=CARTESIAN_POINT('Ctrl Pts',(-2.91096398943488,13.3008719904214,248.941125004055));
#14693=CARTESIAN_POINT('Ctrl Pts',(-0.100094881300308,10.8029187289803,
248.746123345405));
#14694=CARTESIAN_POINT('Ctrl Pts',(1.20409914610878,7.27590390362059,248.551121686755));
#14695=CARTESIAN_POINT('Ctrl Pts',(0.69458281563053,3.55016253464298,248.356120028105));
#14696=CARTESIAN_POINT('Ctrl Pts',(-1.50869278831339,0.502814137742552,
248.161118369455));
#14697=CARTESIAN_POINT('Ctrl Pts',(-4.88702928111861,-1.14873004328783,
247.966116710806));
#14698=CARTESIAN_POINT('Ctrl Pts',(-8.64509371369493,-1.0156610468397,247.771115052156));
#14699=CARTESIAN_POINT('Ctrl Pts',(-11.898157028509,0.870693827689635,247.576113393506));
#14700=CARTESIAN_POINT('Ctrl Pts',(-13.6378083554075,3.67519753547724,247.404974629025));
#14701=CARTESIAN_POINT('Ctrl Pts',(-13.9446027035121,5.66199259233763,247.298836417427));
#14702=CARTESIAN_POINT('Ctrl Pts',(-13.9450882934309,6.43189944074375,247.257698758713));
#14703=CARTESIAN_POINT('Ctrl Pts',(-13.9449455814553,6.43182127881113,249.264720431674));
#14704=CARTESIAN_POINT('Ctrl Pts',(-13.9450750875784,6.9837952416646,249.235228982946));
#14705=CARTESIAN_POINT('Ctrl Pts',(-13.7508600937365,8.75225627081592,249.140736981334));
#14706=CARTESIAN_POINT('Ctrl Pts',(-12.3650517689522,11.4980209748333,248.981244426839));
#14707=CARTESIAN_POINT('Ctrl Pts',(-9.28995072507354,13.6623936974992,248.78624276819));
#14708=CARTESIAN_POINT('Ctrl Pts',(-5.55803537636869,14.1245230511257,248.59124110954));
#14709=CARTESIAN_POINT('Ctrl Pts',(-2.0478787246529,12.7756138638807,248.39623945089));
#14710=CARTESIAN_POINT('Ctrl Pts',(0.414152983126427,9.93322832020636,248.20123779224));
#14711=CARTESIAN_POINT('Ctrl Pts',(1.24844462516442,6.26652501049171,248.006236133591));
#14712=CARTESIAN_POINT('Ctrl Pts',(0.258586022766082,2.63872461703594,247.811234474941));
#14713=CARTESIAN_POINT('Ctrl Pts',(-2.32238882781091,-0.0961107388132638,
247.616232816291));
#14714=CARTESIAN_POINT('Ctrl Pts',(-5.88686308895128,-1.29414212418505,
247.421231157641));
#14715=CARTESIAN_POINT('Ctrl Pts',(-9.59568285503789,-0.673327159893731,
247.226229498991));
#14716=CARTESIAN_POINT('Ctrl Pts',(-12.5757126012294,1.62018083514774,247.031227840341));
#14717=CARTESIAN_POINT('Ctrl Pts',(-13.7982484981895,4.32314964520486,246.877391484569));
#14718=CARTESIAN_POINT('Ctrl Pts',(-13.9453714485852,5.98556064937529,246.78855568168));
#14719=CARTESIAN_POINT('Ctrl Pts',(-13.9450893758793,6.43164617986677,246.764720431674));
#14720=CARTESIAN_POINT('Origin',(-6.5,6.43177298256785,263.507698758713));
#14721=CARTESIAN_POINT('',(-13.9461111697801,6.43178251580015,252.257698758713));
#14722=CARTESIAN_POINT('',(-13.9453632581547,6.4319461154582,251.764720431675));
#14723=CARTESIAN_POINT('',(-13.9455,6.43177298256789,263.507698758713));
#14724=CARTESIAN_POINT('Ctrl Pts',(-13.9461111697801,6.43178251580015,252.257698758713));
#14725=CARTESIAN_POINT('Ctrl Pts',(-13.9461119198476,6.44142059139145,252.257183572842));
#14726=CARTESIAN_POINT('Ctrl Pts',(-13.9437802412465,7.66708591080191,252.191667834088));
#14727=CARTESIAN_POINT('Ctrl Pts',(-13.3237017886373,10.1063878691313,252.061151542451));
#14728=CARTESIAN_POINT('Ctrl Pts',(-10.7908096390754,12.8858146082488,251.866149883801));
#14729=CARTESIAN_POINT('Ctrl Pts',(-7.24776877019554,14.1458213704849,251.671148225152));
#14730=CARTESIAN_POINT('Ctrl Pts',(-3.52868707706655,13.5897755097268,251.476146566502));
#14731=CARTESIAN_POINT('Ctrl Pts',(-0.509116244652642,11.3485821607565,
251.281144907852));
#14732=CARTESIAN_POINT('Ctrl Pts',(1.10007191826787,7.94986635978842,251.086143249202));
#14733=CARTESIAN_POINT('Ctrl Pts',(0.920039966399679,4.19375878202392,250.891141590553));
#14734=CARTESIAN_POINT('Ctrl Pts',(-1.00682871322467,0.964527800673052,
250.696139931903));
#14735=CARTESIAN_POINT('Ctrl Pts',(-4.22690786058867,-0.977596274700365,
250.501138273253));
#14736=CARTESIAN_POINT('Ctrl Pts',(-7.98212170435301,-1.1753957363637,250.306136614603));
#14737=CARTESIAN_POINT('Ctrl Pts',(-11.388412275481,0.417695656017143,250.111134955953));
#14738=CARTESIAN_POINT('Ctrl Pts',(-13.5028831869044,3.23854942376843,249.928322337323));
#14739=CARTESIAN_POINT('Ctrl Pts',(-13.9447188677778,5.44377672635221,249.810510271577));
#14740=CARTESIAN_POINT('Ctrl Pts',(-13.9456747173555,6.43194018529407,249.757698758713));
#14741=CARTESIAN_POINT('Ctrl Pts',(-13.9453632581547,6.4319461154582,251.764720431675));
#14742=CARTESIAN_POINT('Ctrl Pts',(-13.9456687145137,6.76537376641815,251.746902837095));
#14743=CARTESIAN_POINT('Ctrl Pts',(-13.8434001356862,8.31499635810809,251.664084689632));
#14744=CARTESIAN_POINT('Ctrl Pts',(-12.7876966929006,10.9628403258599,251.516265989286));
#14745=CARTESIAN_POINT('Ctrl Pts',(-9.91475940844803,13.3891517385202,251.321264330637));
#14746=CARTESIAN_POINT('Ctrl Pts',(-6.23791443911237,14.1775468064111,251.126262671987));
#14747=CARTESIAN_POINT('Ctrl Pts',(-2.62277003818962,13.142420402497,250.931261013337));
#14748=CARTESIAN_POINT('Ctrl Pts',(0.0795911796349016,10.5274635080144,
250.736259354687));
#14749=CARTESIAN_POINT('Ctrl Pts',(1.23297535983508,6.94829312306938,250.541257696038));
#14750=CARTESIAN_POINT('Ctrl Pts',(0.565851101460774,3.24752280656896,250.346256037388));
#14751=CARTESIAN_POINT('Ctrl Pts',(-1.76472622088437,0.29639335224502,250.151254378738));
#14752=CARTESIAN_POINT('Ctrl Pts',(-5.21008866443971,-1.21033600106685,
249.956252720088));
#14753=CARTESIAN_POINT('Ctrl Pts',(-8.95912393276911,-0.91794881180413,
249.761251061438));
#14754=CARTESIAN_POINT('Ctrl Pts',(-12.1292286261452,1.10472069768431,249.566249402789));
#14755=CARTESIAN_POINT('Ctrl Pts',(-13.6950805877014,3.88592381615938,249.400739192867));
#14756=CARTESIAN_POINT('Ctrl Pts',(-13.9447896499357,5.76721842670446,249.300229535829));
#14757=CARTESIAN_POINT('Ctrl Pts',(-13.9449455814553,6.43182127881113,249.264720431674));
#14758=CARTESIAN_POINT('Origin',(-6.5,6.43177298256785,263.507698758713));
#14759=CARTESIAN_POINT('',(-13.9457314253814,6.43161246431689,254.757698758713));
#14760=CARTESIAN_POINT('',(-13.9459749743085,6.43187801484696,254.264720431675));
#14761=CARTESIAN_POINT('',(-13.9455,6.43177298256789,263.507698758713));
#14762=CARTESIAN_POINT('Ctrl Pts',(-13.9457314253814,6.43161246431689,254.757698758713));
#14763=CARTESIAN_POINT('Ctrl Pts',(-13.9447764467647,7.43903318707587,254.703856874108));
#14764=CARTESIAN_POINT('Ctrl Pts',(-13.4899053046119,9.66349788843306,254.58501443662));
#14765=CARTESIAN_POINT('Ctrl Pts',(-11.3415429435809,12.4836456341042,254.401171446249));
#14766=CARTESIAN_POINT('Ctrl Pts',(-7.92297884889648,14.0502263597522,254.206169787599));
#14767=CARTESIAN_POINT('Ctrl Pts',(-4.16941497964704,13.8232595805219,254.011168128949));
#14768=CARTESIAN_POINT('Ctrl Pts',(-0.964520865428091,11.8561781495442,
253.816166470299));
#14769=CARTESIAN_POINT('Ctrl Pts',(0.937202605263502,8.61207527194551,253.62116481165));
#14770=CARTESIAN_POINT('Ctrl Pts',(1.088048894503,4.85468242098349,253.426163153));
#14771=CARTESIAN_POINT('Ctrl Pts',(-0.547494453099542,1.46857055077819,
253.23116149435));
#14772=CARTESIAN_POINT('Ctrl Pts',(-3.58438541588777,-0.749096899397535,
253.0361598357));
#14773=CARTESIAN_POINT('Ctrl Pts',(-7.3076746545037,-1.27623339504218,252.84115817705));
#14774=CARTESIAN_POINT('Ctrl Pts',(-10.8408199374328,0.0112603133497307,
252.646156518401));
#14775=CARTESIAN_POINT('Ctrl Pts',(-13.3454084612837,2.80288567302779,252.451670045622));
#14776=CARTESIAN_POINT('Ctrl Pts',(-13.9460172844921,5.22539298308426,252.322184125726));
#14777=CARTESIAN_POINT('Ctrl Pts',(-13.9461111697801,6.43178251580015,252.257698758713));
#14778=CARTESIAN_POINT('Ctrl Pts',(-13.9459749743085,6.43187801484696,254.264720431675));
#14779=CARTESIAN_POINT('Ctrl Pts',(-13.9460556454763,6.54682096936603,254.258576691244));
#14780=CARTESIAN_POINT('Ctrl Pts',(-13.9158492372516,7.87781383709142,254.187432397931));
#14781=CARTESIAN_POINT('Ctrl Pts',(-13.1616603427751,10.3925787653421,254.051287551734));
#14782=CARTESIAN_POINT('Ctrl Pts',(-10.5131299782381,13.0620436217747,253.856285893084));
#14783=CARTESIAN_POINT('Ctrl Pts',(-6.91982264875327,14.1706004076339,253.661284234434));
#14784=CARTESIAN_POINT('Ctrl Pts',(-3.2276800535143,13.4572710531101,253.466282575784));
#14785=CARTESIAN_POINT('Ctrl Pts',(-0.305911835418159,11.0899886045361,
253.271280917135));
#14786=CARTESIAN_POINT('Ctrl Pts',(1.15763503213971,7.62606217949973,253.076279258485));
#14787=CARTESIAN_POINT('Ctrl Pts',(0.818410191934892,3.88097443428047,252.881277599835));
#14788=CARTESIAN_POINT('Ctrl Pts',(-1.24372554496956,0.736399436894482,
252.686275941185));
#14789=CARTESIAN_POINT('Ctrl Pts',(-4.54330114888175,-1.06736233941388,
252.491274282535));
#14790=CARTESIAN_POINT('Ctrl Pts',(-8.30352567567975,-1.10566664296319,
252.296272623886));
#14791=CARTESIAN_POINT('Ctrl Pts',(-11.6391615339537,0.630504181754365,
252.101270965236));
#14792=CARTESIAN_POINT('Ctrl Pts',(-13.5706939065415,3.44899169520534,251.924086901166));
#14793=CARTESIAN_POINT('Ctrl Pts',(-13.9445543759801,5.54899287042243,251.811903389978));
#14794=CARTESIAN_POINT('Ctrl Pts',(-13.9453632581547,6.4319461154582,251.764720431675));
#14795=CARTESIAN_POINT('Origin',(-6.5,6.43177298256785,263.507698758713));
#14796=CARTESIAN_POINT('',(-13.9451274702829,6.4316349637354,257.257698758713));
#14797=CARTESIAN_POINT('',(-13.9459987791106,6.43167704459545,256.764720431675));
#14798=CARTESIAN_POINT('',(-13.9455,6.43177298256789,263.507698758713));
#14799=CARTESIAN_POINT('Ctrl Pts',(-13.9451274702829,6.4316349637354,257.257698758713));
#14800=CARTESIAN_POINT('Ctrl Pts',(-13.9445812522303,7.22081373064257,257.215530728257));
#14801=CARTESIAN_POINT('Ctrl Pts',(-13.6267827690106,9.22691426686787,257.108362144918));
#14802=CARTESIAN_POINT('Ctrl Pts',(-11.8547914355129,12.034620997221,256.936193008696));
#14803=CARTESIAN_POINT('Ctrl Pts',(-8.58717183770218,13.8956470450103,256.741191350046));
#14804=CARTESIAN_POINT('Ctrl Pts',(-4.82818696338679,13.9995164531848,256.546189691396));
#14805=CARTESIAN_POINT('Ctrl Pts',(-1.46278287172395,12.3217767520604,256.351188032747));
#14806=CARTESIAN_POINT('Ctrl Pts',(0.716752195883785,9.25740360642712,256.156186374097));
#14807=CARTESIAN_POINT('Ctrl Pts',(1.19730882121199,5.52781638254676,255.961184715447));
#14808=CARTESIAN_POINT('Ctrl Pts',(-0.134246313555596,2.01103993266644,
255.766183056797));
#14809=CARTESIAN_POINT('Ctrl Pts',(-2.96443655298958,-0.465001028602228,
255.571181398147));
#14810=CARTESIAN_POINT('Ctrl Pts',(-6.62697433982785,-1.31739330731701,
255.376179739498));
#14811=CARTESIAN_POINT('Ctrl Pts',(-10.2596196416587,-0.345465453031489,
255.181178080848));
#14812=CARTESIAN_POINT('Ctrl Pts',(-13.0071697546051,2.22196984587269,254.986176422198));
#14813=CARTESIAN_POINT('Ctrl Pts',(-13.8871469687636,4.79794250018219,254.845016648153));
#14814=CARTESIAN_POINT('Ctrl Pts',(-13.9459293435947,6.22282568531489,254.768857426991));
#14815=CARTESIAN_POINT('Ctrl Pts',(-13.9457314253814,6.43161246431689,254.757698758713));
#14816=CARTESIAN_POINT('Ctrl Pts',(-13.9459987791106,6.43167704459545,256.764720431675));
#14817=CARTESIAN_POINT('Ctrl Pts',(-13.9452724247665,7.54429640133474,256.70524999251));
#14818=CARTESIAN_POINT('Ctrl Pts',(-13.4158824236672,9.87366517330999,256.580779000462));
#14819=CARTESIAN_POINT('Ctrl Pts',(-11.0804296656676,12.6836019176416,256.391307455531));
#14820=CARTESIAN_POINT('Ctrl Pts',(-7.59848046310273,14.1037376364226,256.196305796881));
#14821=CARTESIAN_POINT('Ctrl Pts',(-3.85792537225687,13.7177281451327,256.001304138232));
#14822=CARTESIAN_POINT('Ctrl Pts',(-0.739371378738949,11.616448368688,255.806302479582));
#14823=CARTESIAN_POINT('Ctrl Pts',(1.02300694803562,8.29458468304415,255.611300820932));
#14824=CARTESIAN_POINT('Ctrl Pts',(1.01430790860051,4.53417512584038,255.416299162282));
#14825=CARTESIAN_POINT('Ctrl Pts',(-0.763420556208652,1.22050084837849,
255.221297503632));
#14826=CARTESIAN_POINT('Ctrl Pts',(-3.89166299529113,-0.866328074636114,
255.026295844983));
#14827=CARTESIAN_POINT('Ctrl Pts',(-7.63396397027625,-1.23502730735099,
254.831294186333));
#14828=CARTESIAN_POINT('Ctrl Pts',(-11.1093054787138,0.201202866177523,
254.636292527683));
#14829=CARTESIAN_POINT('Ctrl Pts',(-13.4242112656194,3.01277957123129,254.447434609464));
#14830=CARTESIAN_POINT('Ctrl Pts',(-13.9452021474203,5.33072864278933,254.323577244128));
#14831=CARTESIAN_POINT('Ctrl Pts',(-13.9459749743085,6.43187801484696,254.264720431675));
#14832=CARTESIAN_POINT('Ctrl Pts',(-9.81139348551471,-0.236820829780501,
259.706335652578));
#14833=CARTESIAN_POINT('Ctrl Pts',(-10.9008030290343,0.304142342813418,
259.641335099694));
#14834=CARTESIAN_POINT('Ctrl Pts',(-12.8083812201165,1.9297800108904,259.511333993928));
#14835=CARTESIAN_POINT('Ctrl Pts',(-14.1851462695771,5.42940748028812,259.316332335278));
#14836=CARTESIAN_POINT('Ctrl Pts',(-13.7523257580445,9.16467808570731,259.121330676628));
#14837=CARTESIAN_POINT('Ctrl Pts',(-11.6122793516618,12.2567796777562,258.926329017979));
#14838=CARTESIAN_POINT('Ctrl Pts',(-8.26862653170071,13.9774677413128,258.731327359329));
#14839=CARTESIAN_POINT('Ctrl Pts',(-4.50862938937823,13.9217796100182,258.536325700679));
#14840=CARTESIAN_POINT('Ctrl Pts',(-1.21743004662297,12.1027648942659,258.341324042029));
#14841=CARTESIAN_POINT('Ctrl Pts',(0.830132802421682,8.94868564322478,258.146322383379));
#14842=CARTESIAN_POINT('Ctrl Pts',(1.15202784967473,5.20206719240598,257.951320724729));
#14843=CARTESIAN_POINT('Ctrl Pts',(-0.327530058757188,1.74494971672666,
257.75631906608));
#14844=CARTESIAN_POINT('Ctrl Pts',(-3.26021932302907,-0.608789762765702,
257.56131740743));
#14845=CARTESIAN_POINT('Ctrl Pts',(-6.95562279721707,-1.30502921472525,
257.36631574878));
#14846=CARTESIAN_POINT('Ctrl Pts',(-10.5437627550554,-0.179859485232368,
257.17131409013));
#14847=CARTESIAN_POINT('Ctrl Pts',(-13.1799141928899,2.50183057058523,256.976312431481));
#14848=CARTESIAN_POINT('Ctrl Pts',(-14.2434703748362,6.10871341464289,256.781310772831));
#14849=CARTESIAN_POINT('Ctrl Pts',(-13.4840473786807,9.79165143481236,256.586309114181));
#14850=CARTESIAN_POINT('Ctrl Pts',(-11.0804296656676,12.6836019176416,256.391307455531));
#14851=CARTESIAN_POINT('Ctrl Pts',(-7.59848046310273,14.1037376364226,256.196305796881));
#14852=CARTESIAN_POINT('Ctrl Pts',(-3.85792537225687,13.7177281451327,256.001304138232));
#14853=CARTESIAN_POINT('Ctrl Pts',(-0.739371378738949,11.616448368688,255.806302479582));
#14854=CARTESIAN_POINT('Ctrl Pts',(1.02300694803562,8.29458468304415,255.611300820932));
#14855=CARTESIAN_POINT('Ctrl Pts',(1.01430790860051,4.53417512584038,255.416299162282));
#14856=CARTESIAN_POINT('Ctrl Pts',(-0.763420556208652,1.22050084837849,
255.221297503632));
#14857=CARTESIAN_POINT('Ctrl Pts',(-3.89166299529113,-0.866328074636114,
255.026295844983));
#14858=CARTESIAN_POINT('Ctrl Pts',(-7.63396397027625,-1.23502730735099,
254.831294186333));
#14859=CARTESIAN_POINT('Ctrl Pts',(-11.1093054787138,0.201202866177523,
254.636292527683));
#14860=CARTESIAN_POINT('Ctrl Pts',(-13.4995175085847,3.10424302502025,254.441290869033));
#14861=CARTESIAN_POINT('Ctrl Pts',(-14.2418928265339,6.79065518305518,254.246289210384));
#14862=CARTESIAN_POINT('Ctrl Pts',(-13.1616603427751,10.3925787653421,254.051287551734));
#14863=CARTESIAN_POINT('Ctrl Pts',(-10.5131299782381,13.0620436217747,253.856285893084));
#14864=CARTESIAN_POINT('Ctrl Pts',(-6.91982264875327,14.1706004076339,253.661284234434));
#14865=CARTESIAN_POINT('Ctrl Pts',(-3.2276800535143,13.4572710531101,253.466282575784));
#14866=CARTESIAN_POINT('Ctrl Pts',(-0.305911835418159,11.0899886045361,
253.271280917135));
#14867=CARTESIAN_POINT('Ctrl Pts',(1.15763503213971,7.62606217949973,253.076279258485));
#14868=CARTESIAN_POINT('Ctrl Pts',(0.818410191934892,3.88097443428047,252.881277599835));
#14869=CARTESIAN_POINT('Ctrl Pts',(-1.24372554496956,0.736399436894482,
252.686275941185));
#14870=CARTESIAN_POINT('Ctrl Pts',(-4.54330114888175,-1.06736233941388,
252.491274282535));
#14871=CARTESIAN_POINT('Ctrl Pts',(-8.30352567567975,-1.10566664296319,
252.296272623886));
#14872=CARTESIAN_POINT('Ctrl Pts',(-11.6391615339537,0.630504181754365,
252.101270965236));
#14873=CARTESIAN_POINT('Ctrl Pts',(-13.7649284214359,3.73241824434344,251.906269306586));
#14874=CARTESIAN_POINT('Ctrl Pts',(-14.1803751693297,7.46981837160677,251.711267647936));
#14875=CARTESIAN_POINT('Ctrl Pts',(-12.7876966929006,10.9628403258599,251.516265989286));
#14876=CARTESIAN_POINT('Ctrl Pts',(-9.91475940844803,13.3891517385202,251.321264330637));
#14877=CARTESIAN_POINT('Ctrl Pts',(-6.23791443911237,14.1775468064111,251.126262671987));
#14878=CARTESIAN_POINT('Ctrl Pts',(-2.62277003818962,13.142420402497,250.931261013337));
#14879=CARTESIAN_POINT('Ctrl Pts',(0.0795911796349016,10.5274635080144,
250.736259354687));
#14880=CARTESIAN_POINT('Ctrl Pts',(1.23297535983508,6.94829312306938,250.541257696038));
#14881=CARTESIAN_POINT('Ctrl Pts',(0.565851101460774,3.24752280656896,250.346256037388));
#14882=CARTESIAN_POINT('Ctrl Pts',(-1.76472622088437,0.29639335224502,250.151254378738));
#14883=CARTESIAN_POINT('Ctrl Pts',(-5.21008866443971,-1.21033600106685,
249.956252720088));
#14884=CARTESIAN_POINT('Ctrl Pts',(-8.95912393276911,-0.91794881180413,
249.761251061438));
#14885=CARTESIAN_POINT('Ctrl Pts',(-12.1292286261452,1.10472069768431,249.566249402789));
#14886=CARTESIAN_POINT('Ctrl Pts',(-13.974092032751,4.38149269502769,249.371247744139));
#14887=CARTESIAN_POINT('Ctrl Pts',(-14.0593936945629,8.14094469474752,249.176246085489));
#14888=CARTESIAN_POINT('Ctrl Pts',(-12.3650517689522,11.4980209748333,248.981244426839));
#14889=CARTESIAN_POINT('Ctrl Pts',(-9.28995072507354,13.6623936974992,248.78624276819));
#14890=CARTESIAN_POINT('Ctrl Pts',(-5.55803537636869,14.1245230511257,248.59124110954));
#14891=CARTESIAN_POINT('Ctrl Pts',(-2.0478787246529,12.7756138638807,248.39623945089));
#14892=CARTESIAN_POINT('Ctrl Pts',(0.414152983126427,9.93322832020636,248.20123779224));
#14893=CARTESIAN_POINT('Ctrl Pts',(1.24844462516442,6.26652501049171,248.006236133591));
#14894=CARTESIAN_POINT('Ctrl Pts',(0.258586022766082,2.63872461703594,247.811234474941));
#14895=CARTESIAN_POINT('Ctrl Pts',(-2.32238882781091,-0.0961107388132638,
247.616232816291));
#14896=CARTESIAN_POINT('Ctrl Pts',(-5.88686308895128,-1.29414212418505,
247.421231157641));
#14897=CARTESIAN_POINT('Ctrl Pts',(-9.59568285503789,-0.673327159893731,
247.226229498991));
#14898=CARTESIAN_POINT('Ctrl Pts',(-12.5757126012294,1.62018083514774,247.031227840341));
#14899=CARTESIAN_POINT('Ctrl Pts',(-14.1253887260271,5.04644115309334,246.836226181692));
#14900=CARTESIAN_POINT('Ctrl Pts',(-13.8798855290331,8.79883785724345,246.641224523042));
#14901=CARTESIAN_POINT('Ctrl Pts',(-11.8969968350143,11.9939777077968,246.446222864392));
#14902=CARTESIAN_POINT('Ctrl Pts',(-8.64354351795149,13.8796529333669,246.251221205742));
#14903=CARTESIAN_POINT('Ctrl Pts',(-4.88544464111068,14.0119423198044,246.056219547092));
#14904=CARTESIAN_POINT('Ctrl Pts',(-1.50746712882826,12.3596870112171,245.861217888443));
#14905=CARTESIAN_POINT('Ctrl Pts',(0.695205395144706,9.31189841214496,245.666216229793));
#14906=CARTESIAN_POINT('Ctrl Pts',(1.20387608653361,5.58602334650667,245.471214571143));
#14907=CARTESIAN_POINT('Ctrl Pts',(-0.100899992062858,2.05939046574996,
245.276212912493));
#14908=CARTESIAN_POINT('Ctrl Pts',(-2.91261395215861,-0.438036016167426,
245.081211253844));
#14909=CARTESIAN_POINT('Ctrl Pts',(-5.34941510741743,-1.02416954420736,
244.951210148077));
#14910=CARTESIAN_POINT('Ctrl Pts',(-6.56569596473014,-1.01343717499105,
244.886209595194));
#14911=CARTESIAN_POINT('Ctrl Pts',(-10.02198307861,-0.66091312313178,259.432960300116));
#14912=CARTESIAN_POINT('Ctrl Pts',(-11.1806741235541,-0.0855471485469646,
259.367959747233));
#14913=CARTESIAN_POINT('Ctrl Pts',(-13.2095656278426,1.64347369538583,259.237958641467));
#14914=CARTESIAN_POINT('Ctrl Pts',(-14.6738866844109,5.36566158473652,259.042956982817));
#14915=CARTESIAN_POINT('Ctrl Pts',(-14.2135407532006,9.33847844382113,258.847955324167));
#14916=CARTESIAN_POINT('Ctrl Pts',(-11.9373971104438,12.6272236600504,258.652953665517));
#14917=CARTESIAN_POINT('Ctrl Pts',(-8.38110315016291,14.4573396731194,258.457952006867));
#14918=CARTESIAN_POINT('Ctrl Pts',(-4.38198725867788,14.3981100294794,258.262950348218));
#14919=CARTESIAN_POINT('Ctrl Pts',(-0.881482578632365,12.4634142355041,
258.067948689568));
#14920=CARTESIAN_POINT('Ctrl Pts',(1.29629597238295,9.10874986252786,257.872947030918));
#14921=CARTESIAN_POINT('Ctrl Pts',(1.63866208334889,5.12386348659151,257.677945372268));
#14922=CARTESIAN_POINT('Ctrl Pts',(0.0650110086229034,1.44688903357902,
257.482943713618));
#14923=CARTESIAN_POINT('Ctrl Pts',(-3.0541839794597,-1.05653759164428,257.287942054969));
#14924=CARTESIAN_POINT('Ctrl Pts',(-6.98459833874984,-1.79705471206167,
257.092940396319));
#14925=CARTESIAN_POINT('Ctrl Pts',(-10.8009277089898,-0.600329295655229,
256.897938737669));
#14926=CARTESIAN_POINT('Ctrl Pts',(-13.604726411053,2.25190407376516,256.702937079019));
#14927=CARTESIAN_POINT('Ctrl Pts',(-14.7359199379931,6.08816829270179,256.50793542037));
#14928=CARTESIAN_POINT('Ctrl Pts',(-13.9282010868005,10.0053244516867,256.31293376172));
#14929=CARTESIAN_POINT('Ctrl Pts',(-11.3717241988344,13.0811898567669,256.11793210307));
#14930=CARTESIAN_POINT('Ctrl Pts',(-7.66833883383393,14.5916397603364,255.92293044442));
#14931=CARTESIAN_POINT('Ctrl Pts',(-3.68990142003924,14.1810818177503,255.72792878577));
#14932=CARTESIAN_POINT('Ctrl Pts',(-0.373021549692262,11.9461701866086,
255.532927127121));
#14933=CARTESIAN_POINT('Ctrl Pts',(1.50143603807589,8.41305105067232,255.337925468471));
#14934=CARTESIAN_POINT('Ctrl Pts',(1.49218377922334,4.41349651659178,255.142923809821));
#14935=CARTESIAN_POINT('Ctrl Pts',(-0.398600145674072,0.889087598020738,
254.947922151171));
#14936=CARTESIAN_POINT('Ctrl Pts',(-3.72578460274132,-1.33045417101461,
254.752920492521));
#14937=CARTESIAN_POINT('Ctrl Pts',(-7.70607893098081,-1.7226010011629,254.557918833872));
#14938=CARTESIAN_POINT('Ctrl Pts',(-11.4024363825041,-0.195033108587213,
254.362917175222));
#14939=CARTESIAN_POINT('Ctrl Pts',(-13.9446550467372,2.89262722555766,254.167915516572));
#14940=CARTESIAN_POINT('Ctrl Pts',(-14.7342420647803,6.81347846180485,253.972913857922));
#14941=CARTESIAN_POINT('Ctrl Pts',(-13.5853116989371,10.6444680324354,253.777912199273));
#14942=CARTESIAN_POINT('Ctrl Pts',(-10.7683468266292,13.4836987352882,253.582910540623));
#14943=CARTESIAN_POINT('Ctrl Pts',(-6.94652146336407,14.6627547002629,253.387908881973));
#14944=CARTESIAN_POINT('Ctrl Pts',(-3.01957536012084,13.9040608370604,253.192907223323));
#14945=CARTESIAN_POINT('Ctrl Pts',(0.0880040528270217,11.3862299714022,
252.997905564673));
#14946=CARTESIAN_POINT('Ctrl Pts',(1.64462585716397,7.70201355076388,252.802903906023));
#14947=CARTESIAN_POINT('Ctrl Pts',(1.28382785708581,3.71875522635433,252.607902247374));
#14948=CARTESIAN_POINT('Ctrl Pts',(-0.909450351301318,0.374199534419655,
252.412900588724));
#14949=CARTESIAN_POINT('Ctrl Pts',(-4.41886398468801,-1.54427330240607,
252.217898930074));
#14950=CARTESIAN_POINT('Ctrl Pts',(-8.41822172126895,-1.5850135857728,252.022897271424));
#14951=CARTESIAN_POINT('Ctrl Pts',(-11.9659888774937,0.261569821780531,
251.827895612775));
#14952=CARTESIAN_POINT('Ctrl Pts',(-14.2269448887718,3.56075153713113,251.632893954125));
#14953=CARTESIAN_POINT('Ctrl Pts',(-14.6688121638469,7.53583334598187,251.437892295475));
#14954=CARTESIAN_POINT('Ctrl Pts',(-13.1875656585965,11.2509956394116,251.242890636825));
#14955=CARTESIAN_POINT('Ctrl Pts',(-10.1319226049963,13.8316094433007,251.047888978176));
#14956=CARTESIAN_POINT('Ctrl Pts',(-6.2212469872179,14.6701428584681,250.852887319526));
#14957=CARTESIAN_POINT('Ctrl Pts',(-2.37619581390419,13.5691871143815,250.657885660876));
#14958=CARTESIAN_POINT('Ctrl Pts',(0.498023309586833,10.7879308324116,250.462884002226));
#14959=CARTESIAN_POINT('Ctrl Pts',(1.72475748768169,6.98114145918213,250.267882343576));
#14960=CARTESIAN_POINT('Ctrl Pts',(1.01520715498863,3.04501895077211,250.072880684927));
#14961=CARTESIAN_POINT('Ctrl Pts',(-1.46358430504108,-0.0937889397377692,
249.877879026277));
#14962=CARTESIAN_POINT('Ctrl Pts',(-5.12805615925029,-1.69633943988909,
249.682877367627));
#14963=CARTESIAN_POINT('Ctrl Pts',(-9.1155130513194,-1.38535775272618,249.487875708977));
#14964=CARTESIAN_POINT('Ctrl Pts',(-12.4872220120131,0.765944355344317,
249.292874050327));
#14965=CARTESIAN_POINT('Ctrl Pts',(-14.449410356236,4.25110417630493,249.097872391678));
#14966=CARTESIAN_POINT('Ctrl Pts',(-14.5401368164991,8.24964025659253,248.902870733028));
#14967=CARTESIAN_POINT('Ctrl Pts',(-12.7380424361471,11.8202113481242,248.707869074378));
#14968=CARTESIAN_POINT('Ctrl Pts',(-9.46737892577495,14.1222283504466,248.512867415728));
#14969=CARTESIAN_POINT('Ctrl Pts',(-5.49813070249999,14.613747033056,248.317865757078));
#14970=CARTESIAN_POINT('Ctrl Pts',(-1.76474402263465,13.1790533450843,248.122864098429));
#14971=CARTESIAN_POINT('Ctrl Pts',(0.853861724985316,10.1559049842816,247.927862439779));
#14972=CARTESIAN_POINT('Ctrl Pts',(1.74121052806084,6.25601598963642,247.732860781129));
#14973=CARTESIAN_POINT('Ctrl Pts',(0.688401412166355,2.39750396011843,247.537859122479));
#14974=CARTESIAN_POINT('Ctrl Pts',(-2.0567117221724,-0.511254509154269,
247.34285746383));
#14975=CARTESIAN_POINT('Ctrl Pts',(-5.84787036483852,-1.78547525198674,
247.14785580518));
#14976=CARTESIAN_POINT('Ctrl Pts',(-9.79255423128669,-1.12517927425215,
246.95285414653));
#14977=CARTESIAN_POINT('Ctrl Pts',(-12.9621003410296,1.31418541753933,246.75785248788));
#14978=CARTESIAN_POINT('Ctrl Pts',(-14.6103288323697,4.95834033766709,246.56285082923));
#14979=CARTESIAN_POINT('Ctrl Pts',(-14.3492127465467,8.94937243761533,246.367849170581));
#14980=CARTESIAN_POINT('Ctrl Pts',(-12.2402213332185,12.3477086778318,246.172847511931));
#14981=CARTESIAN_POINT('Ctrl Pts',(-8.77986315474553,14.3533042874336,245.977845853281));
#14982=CARTESIAN_POINT('Ctrl Pts',(-4.78276624980934,14.4940066783003,245.782844194631));
#14983=CARTESIAN_POINT('Ctrl Pts',(-1.18996470259768,12.7366754327557,245.587842535981));
#14984=CARTESIAN_POINT('Ctrl Pts',(1.15278779452702,9.49506131469077,245.392840877332));
#14985=CARTESIAN_POINT('Ctrl Pts',(1.6938076326989,5.5322375090646,245.197839218682));
#14986=CARTESIAN_POINT('Ctrl Pts',(0.306053718736717,1.78132678678773,245.002837560032));
#14987=CARTESIAN_POINT('Ctrl Pts',(-2.68447248501027,-0.874924681925421,
244.807835901382));
#14988=CARTESIAN_POINT('Ctrl Pts',(-5.27624313150744,-1.49833364150479,
244.677834795616));
#14989=CARTESIAN_POINT('Ctrl Pts',(-6.56987392984997,-1.48691874232758,
244.612834242732));
#14990=CARTESIAN_POINT('Ctrl Pts',(-10.2325726717054,-1.08500541648306,
259.159584947655));
#14991=CARTESIAN_POINT('Ctrl Pts',(-11.460545218074,-0.475236639907348,
259.094584394772));
#14992=CARTESIAN_POINT('Ctrl Pts',(-13.6107500355688,1.35716737988126,258.964583289005));
#14993=CARTESIAN_POINT('Ctrl Pts',(-15.1626270992447,5.30191568918491,258.769581630356));
#14994=CARTESIAN_POINT('Ctrl Pts',(-14.6747557483566,9.51227880193497,258.574579971706));
#14995=CARTESIAN_POINT('Ctrl Pts',(-12.2625148692259,12.9976676423447,258.379578313056));
#14996=CARTESIAN_POINT('Ctrl Pts',(-8.49357976862511,14.9372116049259,258.184576654406));
#14997=CARTESIAN_POINT('Ctrl Pts',(-4.25534512797754,14.8744404489405,257.989574995756));
#14998=CARTESIAN_POINT('Ctrl Pts',(-0.545535110641766,12.8240635767423,
257.794573337107));
#14999=CARTESIAN_POINT('Ctrl Pts',(1.76245914234423,9.26881408183094,257.599571678457));
#15000=CARTESIAN_POINT('Ctrl Pts',(2.12529631702305,5.04565978077704,257.404570019807));
#15001=CARTESIAN_POINT('Ctrl Pts',(0.457552076003,1.14882835043138,257.209568361157));
#15002=CARTESIAN_POINT('Ctrl Pts',(-2.84814863589033,-1.50428542052285,
257.014566702508));
#15003=CARTESIAN_POINT('Ctrl Pts',(-7.01357388028262,-2.28908020939808,
256.819565043858));
#15004=CARTESIAN_POINT('Ctrl Pts',(-11.0580926629242,-1.02079910607809,
256.624563385208));
#15005=CARTESIAN_POINT('Ctrl Pts',(-14.0295386292161,2.0019775769451,256.429561726558));
#15006=CARTESIAN_POINT('Ctrl Pts',(-15.22836950115,6.06762317076068,256.234560067908));
#15007=CARTESIAN_POINT('Ctrl Pts',(-14.3723547949202,10.218997468561,256.039558409258));
#15008=CARTESIAN_POINT('Ctrl Pts',(-11.6630187320013,13.4787777958922,255.844556750609));
#15009=CARTESIAN_POINT('Ctrl Pts',(-7.73819720456513,15.0795418842502,255.649555091959));
#15010=CARTESIAN_POINT('Ctrl Pts',(-3.52187746782161,14.644435490368,255.454553433309));
#15011=CARTESIAN_POINT('Ctrl Pts',(-0.00667172064557749,12.2758920045292,
255.259551774659));
#15012=CARTESIAN_POINT('Ctrl Pts',(1.97986512811616,8.53151741830049,255.06455011601));
#15013=CARTESIAN_POINT('Ctrl Pts',(1.97005964984618,4.29281790734318,254.86954845736));
#15014=CARTESIAN_POINT('Ctrl Pts',(-0.0337797351394938,0.557674347662983,
254.67454679871));
#15015=CARTESIAN_POINT('Ctrl Pts',(-3.5599062101915,-1.7945802673931,254.47954514006));
#15016=CARTESIAN_POINT('Ctrl Pts',(-7.77819389168537,-2.21017469497481,
254.28454348141));
#15017=CARTESIAN_POINT('Ctrl Pts',(-11.6955672862944,-0.591269083351945,
254.089541822761));
#15018=CARTESIAN_POINT('Ctrl Pts',(-14.3897925848898,2.68101142609504,253.894540164111));
#15019=CARTESIAN_POINT('Ctrl Pts',(-15.2265913030267,6.83630174055454,253.699538505461));
#15020=CARTESIAN_POINT('Ctrl Pts',(-14.0089630550991,10.8963572995288,253.504536846811));
#15021=CARTESIAN_POINT('Ctrl Pts',(-11.0235636750202,13.9053538488017,253.309535188162));
#15022=CARTESIAN_POINT('Ctrl Pts',(-6.97322027797486,15.1549089928918,253.114533529512));
#15023=CARTESIAN_POINT('Ctrl Pts',(-2.81147066672739,14.3508506210107,252.919531870862));
#15024=CARTESIAN_POINT('Ctrl Pts',(0.481919941072204,11.6824713382684,252.724530212212));
#15025=CARTESIAN_POINT('Ctrl Pts',(2.13161668218823,7.77796492202803,252.529528553562));
#15026=CARTESIAN_POINT('Ctrl Pts',(1.74924552223673,3.55653601842819,252.334526894913));
#15027=CARTESIAN_POINT('Ctrl Pts',(-0.575175157633071,0.0119996319448261,
252.139525236263));
#15028=CARTESIAN_POINT('Ctrl Pts',(-4.29442682049427,-2.02118426539827,
251.944523577613));
#15029=CARTESIAN_POINT('Ctrl Pts',(-8.53291776685814,-2.0643605285824,251.749521918963));
#15030=CARTESIAN_POINT('Ctrl Pts',(-12.2928162210337,-0.107364538193309,
251.554520260313));
#15031=CARTESIAN_POINT('Ctrl Pts',(-14.6889613561078,3.38908482991881,251.359518601664));
#15032=CARTESIAN_POINT('Ctrl Pts',(-15.1572491583641,7.601848320357,251.164516943014));
#15033=CARTESIAN_POINT('Ctrl Pts',(-13.5874346242923,11.5391509529632,250.969515284364));
#15034=CARTESIAN_POINT('Ctrl Pts',(-10.3490858015446,14.2740671480813,250.774513625714));
#15035=CARTESIAN_POINT('Ctrl Pts',(-6.20457953532343,15.162738910525,250.579511967064));
#15036=CARTESIAN_POINT('Ctrl Pts',(-2.12962158961875,13.9959538262661,250.384510308415));
#15037=CARTESIAN_POINT('Ctrl Pts',(0.916455439538768,11.0483981568087,250.189508649765));
#15038=CARTESIAN_POINT('Ctrl Pts',(2.2165396155283,7.01398979529488,249.994506991115));
#15039=CARTESIAN_POINT('Ctrl Pts',(1.46456320851649,2.84251509497526,249.799505332465));
#15040=CARTESIAN_POINT('Ctrl Pts',(-1.16244238919778,-0.483971231720556,
249.604503673815));
#15041=CARTESIAN_POINT('Ctrl Pts',(-5.04602365406088,-2.18234287871134,
249.409502015166));
#15042=CARTESIAN_POINT('Ctrl Pts',(-9.27190216986969,-1.85276669364823,
249.214500356516));
#15043=CARTESIAN_POINT('Ctrl Pts',(-12.845215397881,0.427168013004334,249.019498697866));
#15044=CARTESIAN_POINT('Ctrl Pts',(-14.924728679721,4.12071565758218,248.824497039216));
#15045=CARTESIAN_POINT('Ctrl Pts',(-15.0208799384352,8.35833581843755,248.629495380566));
#15046=CARTESIAN_POINT('Ctrl Pts',(-13.1110331033419,12.1424017214152,248.434493721917));
#15047=CARTESIAN_POINT('Ctrl Pts',(-9.64480712647635,14.582063003394,248.239492063267));
#15048=CARTESIAN_POINT('Ctrl Pts',(-5.43822602863129,15.1029710149863,248.044490404617));
#15049=CARTESIAN_POINT('Ctrl Pts',(-1.48160932061641,13.5824928262879,247.849488745967));
#15050=CARTESIAN_POINT('Ctrl Pts',(1.2935704668442,10.3785816483567,247.654487087318));
#15051=CARTESIAN_POINT('Ctrl Pts',(2.23397643095727,6.24550696878113,247.459485428668));
#15052=CARTESIAN_POINT('Ctrl Pts',(1.11821680156663,2.15628330320092,247.264483770018));
#15053=CARTESIAN_POINT('Ctrl Pts',(-1.79103461653389,-0.926398279495272,
247.069482111368));
#15054=CARTESIAN_POINT('Ctrl Pts',(-5.80887764072575,-2.27680837978843,
246.874480452719));
#15055=CARTESIAN_POINT('Ctrl Pts',(-9.98942560753549,-1.57703138861056,
246.679478794069));
#15056=CARTESIAN_POINT('Ctrl Pts',(-13.3484880808298,1.00818999993092,246.484477135419));
#15057=CARTESIAN_POINT('Ctrl Pts',(-15.0952689387123,4.87023952224083,246.289475476769));
#15058=CARTESIAN_POINT('Ctrl Pts',(-14.8185399640602,9.09990701798722,246.094473818119));
#15059=CARTESIAN_POINT('Ctrl Pts',(-12.5834458314227,12.7014396478669,245.899472159469));
#15060=CARTESIAN_POINT('Ctrl Pts',(-8.91618279153957,14.8269556415003,245.70447050082));
#15061=CARTESIAN_POINT('Ctrl Pts',(-4.68008785850801,14.9760710367962,245.50946884217));
#15062=CARTESIAN_POINT('Ctrl Pts',(-0.872462276367092,13.1136638542943,
245.31446718352));
#15063=CARTESIAN_POINT('Ctrl Pts',(1.61037019390933,9.67822421723656,245.11946552487));
#15064=CARTESIAN_POINT('Ctrl Pts',(2.18373917886419,5.47845167162253,244.924463866221));
#15065=CARTESIAN_POINT('Ctrl Pts',(0.713007429536295,1.5032631078255,244.729462207571));
#15066=CARTESIAN_POINT('Ctrl Pts',(-2.45633101786194,-1.31181334768342,
244.534460548921));
#15067=CARTESIAN_POINT('Ctrl Pts',(-5.20307115559744,-1.97249773880223,
244.404459443155));
#15068=CARTESIAN_POINT('Ctrl Pts',(-6.5740518949698,-1.96040030966411,244.339458890271));
#15069=CARTESIAN_POINT('Ctrl Pts',(-10.4431622648007,-1.50909770983434,
258.886209595194));
#15070=CARTESIAN_POINT('Ctrl Pts',(-11.7404163125939,-0.864926131267731,
258.82120904231));
#15071=CARTESIAN_POINT('Ctrl Pts',(-14.011934443295,1.07086106437669,258.691207936544));
#15072=CARTESIAN_POINT('Ctrl Pts',(-15.6513675140784,5.23816979363331,258.496206277894));
#15073=CARTESIAN_POINT('Ctrl Pts',(-15.1359707435126,9.68607916004879,258.301204619244));
#15074=CARTESIAN_POINT('Ctrl Pts',(-12.5876326280079,13.3681116246389,258.106202960595));
#15075=CARTESIAN_POINT('Ctrl Pts',(-8.60605638708732,15.4170835367325,257.911201301945));
#15076=CARTESIAN_POINT('Ctrl Pts',(-4.1287029972772,15.3507708684016,257.716199643295));
#15077=CARTESIAN_POINT('Ctrl Pts',(-0.209587642651167,13.1847129179805,
257.521197984645));
#15078=CARTESIAN_POINT('Ctrl Pts',(2.2286223123055,9.42887830113402,257.326196325996));
#15079=CARTESIAN_POINT('Ctrl Pts',(2.61193055069722,4.96745607496257,257.131194667346));
#15080=CARTESIAN_POINT('Ctrl Pts',(0.850093143383091,0.850767667283733,
256.936193008696));
#15081=CARTESIAN_POINT('Ctrl Pts',(-2.64211329232096,-1.95203324940143,
256.741191350046));
#15082=CARTESIAN_POINT('Ctrl Pts',(-7.04254942181539,-2.7811057067345,256.546189691396));
#15083=CARTESIAN_POINT('Ctrl Pts',(-11.3152576168586,-1.44126891650095,
256.351188032747));
#15084=CARTESIAN_POINT('Ctrl Pts',(-14.4543508473792,1.75205108012504,256.156186374097));
#15085=CARTESIAN_POINT('Ctrl Pts',(-15.720819064307,6.04707804881958,255.961184715447));
#15086=CARTESIAN_POINT('Ctrl Pts',(-14.8165085030399,10.4326704854353,255.766183056797));
#15087=CARTESIAN_POINT('Ctrl Pts',(-11.9543132651681,13.8763657350175,255.571181398147));
#15088=CARTESIAN_POINT('Ctrl Pts',(-7.80805557529633,15.567444008164,255.376179739498));
#15089=CARTESIAN_POINT('Ctrl Pts',(-3.35385351560398,15.1077891629856,255.181178080848));
#15090=CARTESIAN_POINT('Ctrl Pts',(0.359678108401108,12.6056138224498,254.986176422198));
#15091=CARTESIAN_POINT('Ctrl Pts',(2.45829421815644,8.64998378592866,254.791174763548));
#15092=CARTESIAN_POINT('Ctrl Pts',(2.44793552046902,4.17213929809458,254.596173104898));
#15093=CARTESIAN_POINT('Ctrl Pts',(0.331040675395088,0.226261097305232,
254.401171446249));
#15094=CARTESIAN_POINT('Ctrl Pts',(-3.39402781764168,-2.25870636377159,
254.206169787599));
#15095=CARTESIAN_POINT('Ctrl Pts',(-7.85030885238992,-2.69774838878672,
254.011168128949));
#15096=CARTESIAN_POINT('Ctrl Pts',(-11.9886981900848,-0.987505058116681,
253.816166470299));
#15097=CARTESIAN_POINT('Ctrl Pts',(-14.8349301230424,2.46939562663245,253.62116481165));
#15098=CARTESIAN_POINT('Ctrl Pts',(-15.7189405412732,6.85912501930421,253.426163153));
#15099=CARTESIAN_POINT('Ctrl Pts',(-14.432614411261,11.1482465666222,253.23116149435));
#15100=CARTESIAN_POINT('Ctrl Pts',(-11.2787805234113,14.3270089623151,253.0361598357));
#15101=CARTESIAN_POINT('Ctrl Pts',(-6.99991909258566,15.6470632855208,252.84115817705));
#15102=CARTESIAN_POINT('Ctrl Pts',(-2.60336597333394,14.797640404961,252.646156518401));
#15103=CARTESIAN_POINT('Ctrl Pts',(0.875835829317383,11.9787127051345,252.451154859751));
#15104=CARTESIAN_POINT('Ctrl Pts',(2.6186075072125,7.85391629329219,252.256153201101));
#15105=CARTESIAN_POINT('Ctrl Pts',(2.21466318738765,3.39431681050205,252.061151542451));
#15106=CARTESIAN_POINT('Ctrl Pts',(-0.240899963964826,-0.35020027053,251.866149883801));
#15107=CARTESIAN_POINT('Ctrl Pts',(-4.16998965630053,-2.49809522839046,
251.671148225152));
#15108=CARTESIAN_POINT('Ctrl Pts',(-8.64761381244733,-2.54370747139201,
251.476146566502));
#15109=CARTESIAN_POINT('Ctrl Pts',(-12.6196435645737,-0.476298898167143,
251.281144907852));
#15110=CARTESIAN_POINT('Ctrl Pts',(-15.1509778234438,3.2174181227065,251.086143249202));
#15111=CARTESIAN_POINT('Ctrl Pts',(-15.6456861528812,7.66786329473211,250.891141590552));
#15112=CARTESIAN_POINT('Ctrl Pts',(-13.9873035899882,11.8273062665149,250.696139931903));
#15113=CARTESIAN_POINT('Ctrl Pts',(-10.5662489980928,14.7165248528618,250.501138273253));
#15114=CARTESIAN_POINT('Ctrl Pts',(-6.18791208342896,15.6553349625819,250.306136614603));
#15115=CARTESIAN_POINT('Ctrl Pts',(-1.88304736533332,14.4227205381506,250.111134955953));
#15116=CARTESIAN_POINT('Ctrl Pts',(1.3348875694907,11.3088654812059,249.916133297304));
#15117=CARTESIAN_POINT('Ctrl Pts',(2.7083217433749,7.04683813140763,249.721131638654));
#15118=CARTESIAN_POINT('Ctrl Pts',(1.91391926204435,2.6400112391784,249.526129980004));
#15119=CARTESIAN_POINT('Ctrl Pts',(-0.861300473354484,-0.874153523703345,
249.331128321354));
#15120=CARTESIAN_POINT('Ctrl Pts',(-4.96399114887146,-2.66834631753358,
249.136126662704));
#15121=CARTESIAN_POINT('Ctrl Pts',(-9.42829128841997,-2.32017563457029,
248.941125004055));
#15122=CARTESIAN_POINT('Ctrl Pts',(-13.203208783749,0.0883916706643461,
248.746123345405));
#15123=CARTESIAN_POINT('Ctrl Pts',(-15.400047003206,3.99032713885942,248.551121686755));
#15124=CARTESIAN_POINT('Ctrl Pts',(-15.5016230603713,8.46703138028256,248.356120028105));
#15125=CARTESIAN_POINT('Ctrl Pts',(-13.4840237705367,12.4645920947061,248.161118369455));
#15126=CARTESIAN_POINT('Ctrl Pts',(-9.82223532717777,15.0418976563414,247.966116710806));
#15127=CARTESIAN_POINT('Ctrl Pts',(-5.37832135476258,15.5921949969166,247.771115052156));
#15128=CARTESIAN_POINT('Ctrl Pts',(-1.19847461859816,13.9859323074916,247.576113393506));
#15129=CARTESIAN_POINT('Ctrl Pts',(1.73327920870309,10.6012583124319,247.381111734856));
#15130=CARTESIAN_POINT('Ctrl Pts',(2.7267423338537,6.23499794792585,247.186110076207));
#15131=CARTESIAN_POINT('Ctrl Pts',(1.54803219096691,1.9150626462834,246.991108417557));
#15132=CARTESIAN_POINT('Ctrl Pts',(-1.52535751089537,-1.34154204983628,
246.796106758907));
#15133=CARTESIAN_POINT('Ctrl Pts',(-5.76988491661299,-2.76814150759012,
246.601105100257));
#15134=CARTESIAN_POINT('Ctrl Pts',(-10.1862969837843,-2.02888350296897,
246.406103441607));
#15135=CARTESIAN_POINT('Ctrl Pts',(-13.7348758206299,0.702194582322504,
246.211101782958));
#15136=CARTESIAN_POINT('Ctrl Pts',(-15.5802090450549,4.78213870681457,246.016100124308));
#15137=CARTESIAN_POINT('Ctrl Pts',(-15.2878671815738,9.2504415983591,245.821098465658));
#15138=CARTESIAN_POINT('Ctrl Pts',(-12.9266703296268,13.0551706179019,245.626096807008));
#15139=CARTESIAN_POINT('Ctrl Pts',(-9.05250242833362,15.3006069955669,245.431095148358));
#15140=CARTESIAN_POINT('Ctrl Pts',(-4.57740946720667,15.4581353952922,245.236093489709));
#15141=CARTESIAN_POINT('Ctrl Pts',(-0.55495985013651,13.4906522758328,245.041091831059));
#15142=CARTESIAN_POINT('Ctrl Pts',(2.06795259329165,9.86138711978237,244.846090172409));
#15143=CARTESIAN_POINT('Ctrl Pts',(2.67367072502948,5.42466583418046,244.651088513759));
#15144=CARTESIAN_POINT('Ctrl Pts',(1.11996114033587,1.22519942886328,244.456086855109));
#15145=CARTESIAN_POINT('Ctrl Pts',(-2.22818955071361,-1.74870201344141,
244.26108519646));
#15146=CARTESIAN_POINT('Ctrl Pts',(-5.12989917968745,-2.44666183609966,
244.131084090693));
#15147=CARTESIAN_POINT('Ctrl Pts',(-6.57822986008963,-2.43388187700064,
244.06608353781));
#15148=CARTESIAN_POINT('',(1.35783022118007,10.5382254078893,244.886209595194));
#15149=CARTESIAN_POINT('Ctrl Pts',(1.35783022118005,10.5382254078893,244.886209595194));
#15150=CARTESIAN_POINT('Ctrl Pts',(1.44612453701632,10.3322518660377,244.886209595194));
#15151=CARTESIAN_POINT('Ctrl Pts',(1.52645926284569,10.1232070326722,244.886209595194));
#15152=CARTESIAN_POINT('Ctrl Pts',(1.59855524492759,9.91148368960094,244.886209595194));
#15153=CARTESIAN_POINT('Ctrl Pts',(1.62235034055961,9.84160493838024,244.886209595194));
#15154=CARTESIAN_POINT('Ctrl Pts',(1.64524757363912,9.77143430421354,244.886209595194));
#15155=CARTESIAN_POINT('Ctrl Pts',(1.66723568404851,9.70098564097099,244.886209595194));
#15156=CARTESIAN_POINT('Ctrl Pts',(1.73428193209586,9.48617325089184,244.886209595194));
#15157=CARTESIAN_POINT('Ctrl Pts',(1.79287933654356,9.26877589137054,244.886209595194));
#15158=CARTESIAN_POINT('Ctrl Pts',(1.84297302431785,9.04930371074398,244.886209595194));
#15159=CARTESIAN_POINT('Ctrl Pts',(1.87603200511803,8.90446457176506,244.886209595194));
#15160=CARTESIAN_POINT('Ctrl Pts',(1.90538633684054,8.75872169973192,244.886209595194));
#15161=CARTESIAN_POINT('Ctrl Pts',(1.93100783513905,8.61222265349245,244.886209595194));
#15162=CARTESIAN_POINT('Ctrl Pts',(1.94498351169985,8.53231228826498,244.886209595194));
#15163=CARTESIAN_POINT('Ctrl Pts',(1.95784837163251,8.4521769598324,244.886209595194));
#15164=CARTESIAN_POINT('Ctrl Pts',(1.96959660574002,8.37184087900914,244.886209595194));
#15165=CARTESIAN_POINT('Ctrl Pts',(1.9744444460328,8.33869066375004,244.886209595194));
#15166=CARTESIAN_POINT('Ctrl Pts',(1.9791010319949,8.30551366411067,244.886209595194));
#15167=CARTESIAN_POINT('Ctrl Pts',(1.98356526472234,8.27231899002343,244.886209595194));
#15168=CARTESIAN_POINT('Ctrl Pts',(2.01445345584743,8.04264381398712,244.886209595194));
#15169=CARTESIAN_POINT('Ctrl Pts',(2.03615445359886,7.81201163614733,244.886209595194));
#15170=CARTESIAN_POINT('Ctrl Pts',(2.0486294556759,7.58098506779262,244.886209595194));
#15171=CARTESIAN_POINT('Ctrl Pts',(2.06049372757049,7.36126870983855,244.886209595194));
#15172=CARTESIAN_POINT('Ctrl Pts',(2.06401275803726,7.14119496682215,244.886209595194));
#15173=CARTESIAN_POINT('Ctrl Pts',(2.05910149824557,6.92125450421733,244.886209595194));
#15174=CARTESIAN_POINT('Ctrl Pts',(2.05424336876142,6.70369337093213,244.886209595194));
#15175=CARTESIAN_POINT('Ctrl Pts',(2.04113625189595,6.48626204324774,244.886209595194));
#15176=CARTESIAN_POINT('Ctrl Pts',(2.01964971505158,6.269451442371,244.886209595194));
#15177=CARTESIAN_POINT('Ctrl Pts',(2.01639547174321,6.23661439412089,244.886209595194));
#15178=CARTESIAN_POINT('Ctrl Pts',(2.01294892710205,6.20379162458676,244.886209595194));
#15179=CARTESIAN_POINT('Ctrl Pts',(2.00930953270603,6.17098488517774,244.886209595194));
#15180=CARTESIAN_POINT('Ctrl Pts',(2.00630892643853,6.14393639931019,244.886209595194));
#15181=CARTESIAN_POINT('Ctrl Pts',(2.00317717352014,6.11689875710319,244.886209595194));
#15182=CARTESIAN_POINT('Ctrl Pts',(1.99991584422701,6.08988743774954,244.886209595194));
#15183=CARTESIAN_POINT('Ctrl Pts',(1.97636664962037,5.89484585842114,244.886209595194));
#15184=CARTESIAN_POINT('Ctrl Pts',(1.94604394622207,5.7009870739249,244.886209595194));
#15185=CARTESIAN_POINT('Ctrl Pts',(1.90892370423999,5.50865142732287,244.886209595194));
#15186=CARTESIAN_POINT('Ctrl Pts',(1.86788311620583,5.29600281257819,244.886209595194));
#15187=CARTESIAN_POINT('Ctrl Pts',(1.81853400561323,5.08521528319918,244.886209595194));
#15188=CARTESIAN_POINT('Ctrl Pts',(1.76110289217776,4.87672733760996,244.886209595194));
#15189=CARTESIAN_POINT('Ctrl Pts',(1.70358231321742,4.66791461190828,244.886209595194));
#15190=CARTESIAN_POINT('Ctrl Pts',(1.63795418042196,4.46140801599686,244.886209595194));
#15191=CARTESIAN_POINT('Ctrl Pts',(1.56439908283895,4.2576707604985,244.886209595194));
#15192=CARTESIAN_POINT('Ctrl Pts',(1.49132900904767,4.05527695255748,244.886209595194));
#15193=CARTESIAN_POINT('Ctrl Pts',(1.4104357775497,3.85561551861747,244.886209595194));
#15194=CARTESIAN_POINT('Ctrl Pts',(1.32185571267682,3.65917173235668,244.886209595194));
#15195=CARTESIAN_POINT('Ctrl Pts',(1.24882078352789,3.49720235434942,244.886209595194));
#15196=CARTESIAN_POINT('Ctrl Pts',(1.17055942664986,3.33742078495956,244.886209595194));
#15197=CARTESIAN_POINT('Ctrl Pts',(1.08712975796364,3.18011922062368,244.886209595194));
#15198=CARTESIAN_POINT('Ctrl Pts',(1.06774798914291,3.14357607472478,244.886209595194));
#15199=CARTESIAN_POINT('Ctrl Pts',(1.04808722558642,3.10716685946348,244.886209595194));
#15200=CARTESIAN_POINT('Ctrl Pts',(1.02814808042046,3.07089540111588,244.886209595194));
#15201=CARTESIAN_POINT('Ctrl Pts',(1.016081461071,3.0489449174072,244.886209595194));
#15202=CARTESIAN_POINT('Ctrl Pts',(1.00391674600177,3.02705193333218,244.886209595194));
#15203=CARTESIAN_POINT('Ctrl Pts',(0.991656577595838,3.00522125082147,244.886209595194));
#15204=CARTESIAN_POINT('Ctrl Pts',(0.887876283843254,2.82042814123545,244.886209595194));
#15205=CARTESIAN_POINT('Ctrl Pts',(0.7772079883397,2.64000206338419,244.886209595194));
#15206=CARTESIAN_POINT('Ctrl Pts',(0.65985027631292,2.4643596296731,244.886209595194));
#15207=CARTESIAN_POINT('Ctrl Pts',(0.5432329056121,2.28982522158744,244.886209595194));
#15208=CARTESIAN_POINT('Ctrl Pts',(0.420009851735265,2.12001376445838,244.886209595194));
#15209=CARTESIAN_POINT('Ctrl Pts',(0.290335941433409,1.95536608718829,244.886209595194));
#15210=CARTESIAN_POINT('Ctrl Pts',(0.262431134777017,1.91993520066724,244.886209595194));
#15211=CARTESIAN_POINT('Ctrl Pts',(0.234227468440425,1.88474357202413,244.886209595194));
#15212=CARTESIAN_POINT('Ctrl Pts',(0.205726268029875,1.8497958261869,244.886209595194));
#15213=CARTESIAN_POINT('Ctrl Pts',(0.0722508515782293,1.68613026605338,
244.886209595194));
#15214=CARTESIAN_POINT('Ctrl Pts',(-0.067747844306486,1.52781003253958,
244.886209595194));
#15215=CARTESIAN_POINT('Ctrl Pts',(-0.213892779609048,1.3751614069749,244.886209595194));
#15216=CARTESIAN_POINT('Ctrl Pts',(-0.359010861923027,1.2235853310476,244.886209595194));
#15217=CARTESIAN_POINT('Ctrl Pts',(-0.510189741931271,1.07760112169485,
244.886209595194));
#15218=CARTESIAN_POINT('Ctrl Pts',(-0.667082292412142,0.937574313239984,
244.886209595194));
#15219=CARTESIAN_POINT('Ctrl Pts',(-0.74952988634179,0.863989726799347,
244.886209595194));
#15220=CARTESIAN_POINT('Ctrl Pts',(-0.833555643942435,0.792051099534275,
244.886209595194));
#15221=CARTESIAN_POINT('Ctrl Pts',(-0.919110777044865,0.721817091729095,
244.886209595194));
#15222=CARTESIAN_POINT('Ctrl Pts',(-0.939073282913979,0.705429450892353,
244.886209595194));
#15223=CARTESIAN_POINT('Ctrl Pts',(-0.959119055207817,0.689134631185304,
244.886209595194));
#15224=CARTESIAN_POINT('Ctrl Pts',(-0.979247479859861,0.672933409900972,
244.886209595194));
#15225=CARTESIAN_POINT('Ctrl Pts',(-0.99876603580836,0.65722306746043,244.886209595194));
#15226=CARTESIAN_POINT('Ctrl Pts',(-1.01835549032636,0.641606244551321,
244.886209595194));
#15227=CARTESIAN_POINT('Ctrl Pts',(-1.03801184223114,0.626086015887525,
244.886209595194));
#15228=CARTESIAN_POINT('Ctrl Pts',(-1.20034525043236,0.497911081532396,
244.886209595194));
#15229=CARTESIAN_POINT('Ctrl Pts',(-1.3673109959342,0.376262636287241,244.886209595194));
#15230=CARTESIAN_POINT('Ctrl Pts',(-1.53852458201047,0.261404864848448,
244.886209595194));
#15231=CARTESIAN_POINT('Ctrl Pts',(-1.70927208788747,0.146859760962659,
244.886209595194));
#15232=CARTESIAN_POINT('Ctrl Pts',(-1.88424496013289,0.0390680863175076,
244.886209595194));
#15233=CARTESIAN_POINT('Ctrl Pts',(-2.06308629552965,-0.0616626459374319,
244.886209595194));
#15234=CARTESIAN_POINT('Ctrl Pts',(-2.23946463511152,-0.161006118522091,
244.886209595194));
#15235=CARTESIAN_POINT('Ctrl Pts',(-2.41960621621606,-0.253482007969893,
244.886209595194));
#15236=CARTESIAN_POINT('Ctrl Pts',(-2.60318342048835,-0.338747200573998,
244.886209595194));
#15237=CARTESIAN_POINT('Ctrl Pts',(-2.70012537870016,-0.383773350586004,
244.886209595194));
#15238=CARTESIAN_POINT('Ctrl Pts',(-2.7980255886567,-0.426787896006235,
244.886209595194));
#15239=CARTESIAN_POINT('Ctrl Pts',(-2.89683665674224,-0.467734470423956,
244.886209595194));
#15240=CARTESIAN_POINT('Ctrl Pts',(-3.04097870853666,-0.527465868584872,
244.886209595194));
#15241=CARTESIAN_POINT('Ctrl Pts',(-3.18705923438264,-0.582797331497136,
244.886209595194));
#15242=CARTESIAN_POINT('Ctrl Pts',(-3.33486953849687,-0.633661156473034,
244.886209595194));
#15243=CARTESIAN_POINT('Ctrl Pts',(-3.39953654654684,-0.655914079899989,
244.886209595194));
#15244=CARTESIAN_POINT('Ctrl Pts',(-3.46453462393422,-0.677311646689401,
244.886209595194));
#15245=CARTESIAN_POINT('Ctrl Pts',(-3.52984613578212,-0.697847143289031,
244.886209595194));
#15246=CARTESIAN_POINT('Ctrl Pts',(-3.56516437852512,-0.708952040928562,
244.886209595194));
#15247=CARTESIAN_POINT('Ctrl Pts',(-3.60057427600938,-0.719804834255837,
244.886209595194));
#15248=CARTESIAN_POINT('Ctrl Pts',(-3.63607302111687,-0.730404383715522,
244.886209595194));
#15249=CARTESIAN_POINT('Ctrl Pts',(-3.65875876597319,-0.73717810695296,
244.886209595194));
#15250=CARTESIAN_POINT('Ctrl Pts',(-3.68148075176679,-0.743848346809334,
244.886209595194));
#15251=CARTESIAN_POINT('Ctrl Pts',(-3.70422452712716,-0.750410975276562,
244.886209595194));
#15252=CARTESIAN_POINT('Ctrl Pts',(-3.8972186286978,-0.806098677292012,
244.886209595194));
#15253=CARTESIAN_POINT('Ctrl Pts',(-4.0920279033681,-0.854116647242459,
244.886209595194));
#15254=CARTESIAN_POINT('Ctrl Pts',(-4.28819139577941,-0.894431540392954,
244.886209595194));
#15255=CARTESIAN_POINT('Ctrl Pts',(-4.48469632720638,-0.934816604997193,
244.886209595194));
#15256=CARTESIAN_POINT('Ctrl Pts',(-4.68256091287849,-0.967471782307452,
244.886209595194));
#15257=CARTESIAN_POINT('Ctrl Pts',(-4.88132713130532,-0.992311928479702,
244.886209595194));
#15258=CARTESIAN_POINT('Ctrl Pts',(-5.07865800431528,-1.01697269713878,
244.886209595194));
#15259=CARTESIAN_POINT('Ctrl Pts',(-5.27687821507438,-1.03393085364646,
244.886209595194));
#15260=CARTESIAN_POINT('Ctrl Pts',(-5.47553442148217,-1.04305246810537,
244.886209595194));
#15261=CARTESIAN_POINT('Ctrl Pts',(-5.67013106277854,-1.0519876812004,244.886209595194));
#15262=CARTESIAN_POINT('Ctrl Pts',(-5.86514663500213,-1.05340321878937,
244.886209595194));
#15263=CARTESIAN_POINT('Ctrl Pts',(-6.06014087521336,-1.04712598159856,
244.886209595194));
#15264=CARTESIAN_POINT('Ctrl Pts',(-6.22877466971413,-1.04169733752517,
244.886209595194));
#15265=CARTESIAN_POINT('Ctrl Pts',(-6.39739251603998,-1.03051451432944,
244.886209595194));
#15266=CARTESIAN_POINT('Ctrl Pts',(-6.56569596473014,-1.01343717499105,
244.886209595194));
#15267=CARTESIAN_POINT('Ctrl Pts',(-15.3655110343894,6.43162198763813,245.944594374291));
#15268=CARTESIAN_POINT('Ctrl Pts',(-15.3649309294981,7.34903226064943,245.903429071413));
#15269=CARTESIAN_POINT('Ctrl Pts',(-15.2231421086117,8.26661783103502,245.862263768536));
#15270=CARTESIAN_POINT('Ctrl Pts',(-14.9430580168295,9.13984595302551,245.821098465658));
#15271=CARTESIAN_POINT('Ctrl Pts',(-14.5008015642581,10.5186846048734,245.756097912775));
#15272=CARTESIAN_POINT('Ctrl Pts',(-13.7137359469425,11.7869276113877,245.691097359891));
#15273=CARTESIAN_POINT('Ctrl Pts',(-12.6745084880691,12.7952885109223,245.626096807008));
#15274=CARTESIAN_POINT('Ctrl Pts',(-11.6352810291958,13.8036494104569,245.561096254125));
#15275=CARTESIAN_POINT('Ctrl Pts',(-10.3438917287647,14.5521282030119,245.496095701242));
#15276=CARTESIAN_POINT('Ctrl Pts',(-8.95234825169469,14.952622332577,245.431095148358));
#15277=CARTESIAN_POINT('Ctrl Pts',(-7.56080477462465,15.353116462142,245.366094595475));
#15278=CARTESIAN_POINT('Ctrl Pts',(-6.06910712091566,15.4056259287171,245.301094042592));
#15279=CARTESIAN_POINT('Ctrl Pts',(-4.65285002454947,15.1039668087614,245.236093489709));
#15280=CARTESIAN_POINT('Ctrl Pts',(-3.23659292818328,14.8023076888057,245.171092936825));
#15281=CARTESIAN_POINT('Ctrl Pts',(-1.89577638915989,14.1464799823193,245.106092383942));
#15282=CARTESIAN_POINT('Ctrl Pts',(-0.788216045743495,13.2136886030676,
245.041091831059));
#15283=CARTESIAN_POINT('Ctrl Pts',(0.0914760734497426,12.4728086771505,
244.989464419104));
#15284=CARTESIAN_POINT('Ctrl Pts',(0.82401835200515,11.5572060168434,244.937837007149));
#15285=CARTESIAN_POINT('Ctrl Pts',(1.35783022118007,10.5382254078893,244.886209595194));
#15286=CARTESIAN_POINT('',(-10.823035578903,12.4936896459292,258.886209595194));
#15287=CARTESIAN_POINT('Ctrl Pts',(-10.8232424565741,12.4936870253197,258.886209595194));
#15288=CARTESIAN_POINT('Ctrl Pts',(-10.9962627591582,12.3931877738435,258.886209595194));
#15289=CARTESIAN_POINT('Ctrl Pts',(-11.1648792140985,12.2858828094393,258.886209595194));
#15290=CARTESIAN_POINT('Ctrl Pts',(-11.3286727627758,12.1720546999129,258.886209595194));
#15291=CARTESIAN_POINT('Ctrl Pts',(-11.3719609836911,12.1419716081713,258.886209595194));
#15292=CARTESIAN_POINT('Ctrl Pts',(-11.414912325497,12.1114326134579,258.886209595194));
#15293=CARTESIAN_POINT('Ctrl Pts',(-11.4575189940443,12.0804423304784,258.886209595194));
#15294=CARTESIAN_POINT('Ctrl Pts',(-11.6170775755966,11.9643861880317,258.886209595194));
#15295=CARTESIAN_POINT('Ctrl Pts',(-11.7718036894195,11.8420049310846,258.886209595194));
#15296=CARTESIAN_POINT('Ctrl Pts',(-11.9214743026385,11.7137318538276,258.886209595194));
#15297=CARTESIAN_POINT('Ctrl Pts',(-12.0728964758752,11.5839576268885,258.886209595194));
#15298=CARTESIAN_POINT('Ctrl Pts',(-12.2191446525058,11.4481525108327,258.886209595194));
#15299=CARTESIAN_POINT('Ctrl Pts',(-12.3599656903401,11.3067164015234,258.886209595194));
#15300=CARTESIAN_POINT('Ctrl Pts',(-12.5014891650213,11.1645747872969,258.886209595194));
#15301=CARTESIAN_POINT('Ctrl Pts',(-12.637531758463,11.0167454229121,258.886209595194));
#15302=CARTESIAN_POINT('Ctrl Pts',(-12.7678062758748,10.8635913652864,258.886209595194));
#15303=CARTESIAN_POINT('Ctrl Pts',(-12.8215172612427,10.800447355916,258.886209595194));
#15304=CARTESIAN_POINT('Ctrl Pts',(-12.8742473673171,10.7363977711965,258.886209595194));
#15305=CARTESIAN_POINT('Ctrl Pts',(-12.925974648325,10.6714662234646,258.886209595194));
#15306=CARTESIAN_POINT('Ctrl Pts',(-12.9487466877829,10.6428812343022,258.886209595194));
#15307=CARTESIAN_POINT('Ctrl Pts',(-12.9713243599966,10.6141253035477,258.886209595194));
#15308=CARTESIAN_POINT('Ctrl Pts',(-12.9937057199584,10.5852003868364,258.886209595194));
#15309=CARTESIAN_POINT('Ctrl Pts',(-13.0094132693077,10.5649004784554,258.886209595194));
#15310=CARTESIAN_POINT('Ctrl Pts',(-13.0250248889854,10.5445162521638,258.886209595194));
#15311=CARTESIAN_POINT('Ctrl Pts',(-13.0405290850171,10.52406286367,258.886209595194));
#15312=CARTESIAN_POINT('Ctrl Pts',(-13.1640791364024,10.3610736190649,258.886209595194));
#15313=CARTESIAN_POINT('Ctrl Pts',(-13.28096895391,10.19349218881,258.886209595194));
#15314=CARTESIAN_POINT('Ctrl Pts',(-13.3909685719566,10.0217722607569,258.886209595194));
#15315=CARTESIAN_POINT('Ctrl Pts',(-13.5021881043256,9.84814792973064,258.886209595194));
#15316=CARTESIAN_POINT('Ctrl Pts',(-13.6063643146254,9.67029237005731,258.886209595194));
#15317=CARTESIAN_POINT('Ctrl Pts',(-13.7032312620926,9.48862953956923,258.886209595194));
#15318=CARTESIAN_POINT('Ctrl Pts',(-13.7537935981977,9.39380568754212,258.886209595194));
#15319=CARTESIAN_POINT('Ctrl Pts',(-13.802363935953,9.2979438059089,258.886209595194));
#15320=CARTESIAN_POINT('Ctrl Pts',(-13.8489006720425,9.20110001266742,258.886209595194));
#15321=CARTESIAN_POINT('Ctrl Pts',(-13.9375249912023,9.0166711944459,258.886209595194));
#15322=CARTESIAN_POINT('Ctrl Pts',(-14.0187767861329,8.828682979896,258.886209595194));
#15323=CARTESIAN_POINT('Ctrl Pts',(-14.0926202070319,8.63760482503333,258.886209595194));
#15324=CARTESIAN_POINT('Ctrl Pts',(-14.1425987595604,8.50827970055252,258.886209595194));
#15325=CARTESIAN_POINT('Ctrl Pts',(-14.1891827861434,8.37753843385314,258.886209595194));
#15326=CARTESIAN_POINT('Ctrl Pts',(-14.2323493892896,8.24551998345277,258.886209595194));
#15327=CARTESIAN_POINT('Ctrl Pts',(-14.2701201670426,8.13000383935244,258.886209595194));
#15328=CARTESIAN_POINT('Ctrl Pts',(-14.3052743501943,8.01350973685049,258.886209595194));
#15329=CARTESIAN_POINT('Ctrl Pts',(-14.3377902985068,7.89612836485591,258.886209595194));
#15330=CARTESIAN_POINT('Ctrl Pts',(-14.346429637234,7.86494067126071,258.886209595194));
#15331=CARTESIAN_POINT('Ctrl Pts',(-14.3548838005409,7.83368591534596,258.886209595194));
#15332=CARTESIAN_POINT('Ctrl Pts',(-14.3631450505409,7.80239401210579,258.886209595194));
#15333=CARTESIAN_POINT('Ctrl Pts',(-14.4166320128683,7.59979648149569,258.886209595194));
#15334=CARTESIAN_POINT('Ctrl Pts',(-14.4620953012549,7.39543822996992,258.886209595194));
#15335=CARTESIAN_POINT('Ctrl Pts',(-14.4995572873584,7.18983840967408,258.886209595194));
#15336=CARTESIAN_POINT('Ctrl Pts',(-14.5373634910809,6.98234944552973,258.886209595194));
#15337=CARTESIAN_POINT('Ctrl Pts',(-14.56702093691,6.77359537785523,258.886209595194));
#15338=CARTESIAN_POINT('Ctrl Pts',(-14.5885083677775,6.56407930036393,258.886209595194));
#15339=CARTESIAN_POINT('Ctrl Pts',(-14.6100583701105,6.35395311140345,258.886209595194));
#15340=CARTESIAN_POINT('Ctrl Pts',(-14.6233909328497,6.14305979808593,258.886209595194));
#15341=CARTESIAN_POINT('Ctrl Pts',(-14.6284367109836,5.93188605522641,258.886209595194));
#15342=CARTESIAN_POINT('Ctrl Pts',(-14.6328908783898,5.74547215086212,258.886209595194));
#15343=CARTESIAN_POINT('Ctrl Pts',(-14.6308869777452,5.55883911524171,258.886209595194));
#15344=CARTESIAN_POINT('Ctrl Pts',(-14.6223442849833,5.37231468247016,258.886209595194));
#15345=CARTESIAN_POINT('Ctrl Pts',(-14.6145158995427,5.2013867099297,258.886209595194));
#15346=CARTESIAN_POINT('Ctrl Pts',(-14.6011961461742,5.03054965713793,258.886209595194));
#15347=CARTESIAN_POINT('Ctrl Pts',(-14.5824613743046,4.86003478198579,258.886209595194));
#15348=CARTESIAN_POINT('Ctrl Pts',(-14.5785562001578,4.82449176674548,258.886209595194));
#15349=CARTESIAN_POINT('Ctrl Pts',(-14.5744156684306,4.78896275492112,258.886209595194));
#15350=CARTESIAN_POINT('Ctrl Pts',(-14.5700403476506,4.75344985240902,258.886209595194));
#15351=CARTESIAN_POINT('Ctrl Pts',(-14.5670822017472,4.72943964781649,258.886209595194));
#15352=CARTESIAN_POINT('Ctrl Pts',(-14.5640167675075,4.70543742739751,258.886209595194));
#15353=CARTESIAN_POINT('Ctrl Pts',(-14.5608460966616,4.68145708463058,258.886209595194));
#15354=CARTESIAN_POINT('Ctrl Pts',(-14.5330800108368,4.47145728088453,258.886209595194));
#15355=CARTESIAN_POINT('Ctrl Pts',(-14.4972158831587,4.26287242485888,258.886209595194));
#15356=CARTESIAN_POINT('Ctrl Pts',(-14.4535260619027,4.0561402580423,258.886209595194));
#15357=CARTESIAN_POINT('Ctrl Pts',(-14.4091822964983,3.84631374826656,258.886209595194));
#15358=CARTESIAN_POINT('Ctrl Pts',(-14.3567768109032,3.63839520345404,258.886209595194));
#15359=CARTESIAN_POINT('Ctrl Pts',(-14.2965417977189,3.43283197016907,258.886209595194));
#15360=CARTESIAN_POINT('Ctrl Pts',(-14.2356273487361,3.22495003531564,258.886209595194));
#15361=CARTESIAN_POINT('Ctrl Pts',(-14.1667057060184,3.01947617599251,258.886209595194));
#15362=CARTESIAN_POINT('Ctrl Pts',(-14.0899640341328,2.81687222565179,258.886209595194));
#15363=CARTESIAN_POINT('Ctrl Pts',(-14.0133154717191,2.61451409151968,258.886209595194));
#15364=CARTESIAN_POINT('Ctrl Pts',(-13.9288656987432,2.4150182161233,258.886209595194));
#15365=CARTESIAN_POINT('Ctrl Pts',(-13.8367502112676,2.21885418100079,258.886209595194));
#15366=CARTESIAN_POINT('Ctrl Pts',(-13.7773429727528,2.09234381947636,258.886209595194));
#15367=CARTESIAN_POINT('Ctrl Pts',(-13.7147463578949,1.96721946515344,258.886209595194));
#15368=CARTESIAN_POINT('Ctrl Pts',(-13.6489858644575,1.8436112222596,258.886209595194));
#15369=CARTESIAN_POINT('Ctrl Pts',(-13.6273871639318,1.80301272183439,258.886209595194));
#15370=CARTESIAN_POINT('Ctrl Pts',(-13.6054470896328,1.76257780630002,258.886209595194));
#15371=CARTESIAN_POINT('Ctrl Pts',(-13.5831663497552,1.7223111889938,258.886209595194));
#15372=CARTESIAN_POINT('Ctrl Pts',(-13.5703103265728,1.69907728525407,258.886209595194));
#15373=CARTESIAN_POINT('Ctrl Pts',(-13.5573395664917,1.67589709266456,258.886209595194));
#15374=CARTESIAN_POINT('Ctrl Pts',(-13.5442586020083,1.652779302687,258.886209595194));
#15375=CARTESIAN_POINT('Ctrl Pts',(-13.5109861443909,1.59397739337683,258.886209595194));
#15376=CARTESIAN_POINT('Ctrl Pts',(-13.4770141268117,1.53560253787742,258.886209595194));
#15377=CARTESIAN_POINT('Ctrl Pts',(-13.4423489066022,1.47766813376721,258.886209595194));
#15378=CARTESIAN_POINT('Ctrl Pts',(-13.3304954334553,1.29073251716748,258.886209595194));
#15379=CARTESIAN_POINT('Ctrl Pts',(-13.2114286638561,1.10838157575998,258.886209595194));
#15380=CARTESIAN_POINT('Ctrl Pts',(-13.0855785738617,0.930887529340759,
258.886209595194));
#15381=CARTESIAN_POINT('Ctrl Pts',(-12.9582535083845,0.75131323516952,258.886209595194));
#15382=CARTESIAN_POINT('Ctrl Pts',(-12.8239848789003,0.576709821915435,
258.886209595194));
#15383=CARTESIAN_POINT('Ctrl Pts',(-12.683167458968,0.407377372868322,258.886209595194));
#15384=CARTESIAN_POINT('Ctrl Pts',(-12.6043188879753,0.312562245333209,
258.886209595194));
#15385=CARTESIAN_POINT('Ctrl Pts',(-12.5234162183088,0.219400076748213,
258.886209595194));
#15386=CARTESIAN_POINT('Ctrl Pts',(-12.4405225347237,0.127946949428894,
258.886209595194));
#15387=CARTESIAN_POINT('Ctrl Pts',(-12.3755960071966,0.0563162324484651,
258.886209595194));
#15388=CARTESIAN_POINT('Ctrl Pts',(-12.3094479391927,-0.0142659736946958,
258.886209595194));
#15389=CARTESIAN_POINT('Ctrl Pts',(-12.2421069024936,-0.0837714615598565,
258.886209595194));
#15390=CARTESIAN_POINT('Ctrl Pts',(-12.2202634288917,-0.106317020164007,
258.886209595194));
#15391=CARTESIAN_POINT('Ctrl Pts',(-12.1982941806089,-0.128749454165727,
258.886209595194));
#15392=CARTESIAN_POINT('Ctrl Pts',(-12.1762108309938,-0.15105715093638,
258.886209595194));
#15393=CARTESIAN_POINT('Ctrl Pts',(-12.0183040784386,-0.310568095400722,
258.886209595194));
#15394=CARTESIAN_POINT('Ctrl Pts',(-11.8544368053254,-0.463838871245082,
258.886209595194));
#15395=CARTESIAN_POINT('Ctrl Pts',(-11.6850343963611,-0.610571371251755,
258.886209595194));
#15396=CARTESIAN_POINT('Ctrl Pts',(-11.5148563117381,-0.757975743809088,
258.886209595194));
#15397=CARTESIAN_POINT('Ctrl Pts',(-11.3390918710149,-0.898782372462146,
258.886209595194));
#15398=CARTESIAN_POINT('Ctrl Pts',(-11.1581273042666,-1.03266178326809,
258.886209595194));
#15399=CARTESIAN_POINT('Ctrl Pts',(-10.97782946116,-1.16604794520257,258.886209595194));
#15400=CARTESIAN_POINT('Ctrl Pts',(-10.7923692685769,-1.29255835071171,
258.886209595194));
#15401=CARTESIAN_POINT('Ctrl Pts',(-10.6020908326724,-1.41183230447377,
258.886209595194));
#15402=CARTESIAN_POINT('Ctrl Pts',(-10.5494809025752,-1.44481026301129,
258.886209595194));
#15403=CARTESIAN_POINT('Ctrl Pts',(-10.4965024352886,-1.47723479084939,
258.886209595194));
#15404=CARTESIAN_POINT('Ctrl Pts',(-10.4431622648007,-1.50909770983434,
258.886209595194));
#15405=CARTESIAN_POINT('Ctrl Pts',(-10.8232424565743,12.4936870253196,258.886209595194));
#15406=CARTESIAN_POINT('Ctrl Pts',(-10.0361782840362,13.0538187692527,258.834582183239));
#15407=CARTESIAN_POINT('Ctrl Pts',(-8.01076733182417,13.973648670065,258.7179542184));
#15408=CARTESIAN_POINT('Ctrl Pts',(-4.50862938937823,13.9217796100182,258.536325700679));
#15409=CARTESIAN_POINT('Ctrl Pts',(-1.21743004662297,12.1027648942659,258.341324042029));
#15410=CARTESIAN_POINT('Ctrl Pts',(0.830132802421682,8.94868564322478,258.146322383379));
#15411=CARTESIAN_POINT('Ctrl Pts',(1.15202784967473,5.20206719240598,257.951320724729));
#15412=CARTESIAN_POINT('Ctrl Pts',(-0.327530058757188,1.74494971672666,
257.75631906608));
#15413=CARTESIAN_POINT('Ctrl Pts',(-3.26021932302907,-0.608789762765702,
257.56131740743));
#15414=CARTESIAN_POINT('Ctrl Pts',(-6.95562279721707,-1.30502921472525,
257.36631574878));
#15415=CARTESIAN_POINT('Ctrl Pts',(-10.5437627550554,-0.179859485232368,
257.17131409013));
#15416=CARTESIAN_POINT('Ctrl Pts',(-13.1799141928899,2.50183057058523,256.976312431481));
#15417=CARTESIAN_POINT('Ctrl Pts',(-13.9191133736988,5.00870786476085,256.840781211995));
#15418=CARTESIAN_POINT('Ctrl Pts',(-13.946066322283,6.32821536422246,256.770250545393));
#15419=CARTESIAN_POINT('Ctrl Pts',(-13.9459987791106,6.43167704459545,256.764720431675));
#15420=CARTESIAN_POINT('Origin',(-6.5,6.43177298256785,263.507698758713));
#15421=CARTESIAN_POINT('',(-2.17696442109693,12.4936896459292,258.886209595194));
#15422=CARTESIAN_POINT('Origin',(-6.5,6.43177298256785,258.886209595194));
#15423=CARTESIAN_POINT('Ctrl Pts',(-2.17696442109716,12.4936896459294,258.886209595194));
#15424=CARTESIAN_POINT('Ctrl Pts',(-1.18666420925076,11.7874603644412,258.82120904231));
#15425=CARTESIAN_POINT('Ctrl Pts',(0.440228799577828,9.88095277329113,258.691207936544));
#15426=CARTESIAN_POINT('Ctrl Pts',(1.24700262019175,6.20780816435965,258.496206277894));
#15427=CARTESIAN_POINT('Ctrl Pts',(0.229685845340515,2.58777411101262,258.301204619244));
#15428=CARTESIAN_POINT('Ctrl Pts',(-2.37185181727327,-0.127533036464177,
258.106202960595));
#15429=CARTESIAN_POINT('Ctrl Pts',(-5.94529650349566,-1.29854737465037,
257.911201301945));
#15430=CARTESIAN_POINT('Ctrl Pts',(-9.64930901441413,-0.649724643295287,
257.716199643295));
#15431=CARTESIAN_POINT('Ctrl Pts',(-12.6119171141539,1.66625481118851,257.521197984645));
#15432=CARTESIAN_POINT('Ctrl Pts',(-13.8061465224486,4.36070848620917,257.368364356451));
#15433=CARTESIAN_POINT('Ctrl Pts',(-13.9454232283679,6.00432209899089,257.280531281141));
#15434=CARTESIAN_POINT('Ctrl Pts',(-13.9451274702829,6.4316349637354,257.257698758713));
#15435=CARTESIAN_POINT('Ctrl Pts',(-1.35218810791047,13.6502207882711,259.706335652578));
#15436=CARTESIAN_POINT('Ctrl Pts',(-0.17295210250719,12.8092525779865,259.641335099694));
#15437=CARTESIAN_POINT('Ctrl Pts',(1.7643299358078,10.5390093031041,259.511333993928));
#15438=CARTESIAN_POINT('Ctrl Pts',(2.72502521397086,6.16507872721444,259.316332335278));
#15439=CARTESIAN_POINT('Ctrl Pts',(1.51361825327903,1.85439147760396,259.121330676628));
#15440=CARTESIAN_POINT('Ctrl Pts',(-1.58425736511246,-1.37895929393983,
258.926329017979));
#15441=CARTESIAN_POINT('Ctrl Pts',(-5.83946663084983,-2.77338721984928,
258.731327359329));
#15442=CARTESIAN_POINT('Ctrl Pts',(-10.2501542840368,-2.00077794764538,
258.536325700679));
#15443=CARTESIAN_POINT('Ctrl Pts',(-13.7779876615523,0.757058845512007,
258.341324042029));
#15444=CARTESIAN_POINT('Ctrl Pts',(-15.5924209408393,4.85083377978987,258.146322383379));
#15445=CARTESIAN_POINT('Ctrl Pts',(-15.2663057152418,9.3168008922508,257.951320724729));
#15446=CARTESIAN_POINT('Ctrl Pts',(-12.8764127146944,13.1035680934288,257.75631906608));
#15447=CARTESIAN_POINT('Ctrl Pts',(-8.98537579921665,15.3196525658886,257.56131740743));
#15448=CARTESIAN_POINT('Ctrl Pts',(-4.50922780436335,15.443338842549,257.36631574878));
#15449=CARTESIAN_POINT('Ctrl Pts',(-0.501750445330013,13.4455092555275,
257.17131409013));
#15450=CARTESIAN_POINT('Ctrl Pts',(2.09361023016663,9.7964954472964,256.976312431481));
#15451=CARTESIAN_POINT('Ctrl Pts',(2.66585051492385,5.35535377421556,256.781310772831));
#15452=CARTESIAN_POINT('Ctrl Pts',(1.08025279484469,1.16762427255162,256.586309114181));
#15453=CARTESIAN_POINT('Ctrl Pts',(-2.28989919801298,-1.78081158301322,
256.391307455531));
#15454=CARTESIAN_POINT('Ctrl Pts',(-6.65119931460797,-2.79582869980662,
256.196305796881));
#15455=CARTESIAN_POINT('Ctrl Pts',(-10.9769038671609,-1.63847024757435,
256.001304138232));
#15456=CARTESIAN_POINT('Ctrl Pts',(-14.24864912287,1.41879674055062,255.806302479582));
#15457=CARTESIAN_POINT('Ctrl Pts',(-15.6961959998786,5.65622597281891,255.611300820932));
#15458=CARTESIAN_POINT('Ctrl Pts',(-14.9787608819424,10.0762356231545,255.416299162282));
#15459=CARTESIAN_POINT('Ctrl Pts',(-12.2652434004147,13.6382605157787,255.221297503632));
#15460=CARTESIAN_POINT('Ctrl Pts',(-8.19446383376755,15.5037235086731,255.026295844983));
#15461=CARTESIAN_POINT('Ctrl Pts',(-3.7247710979183,15.2334545590181,254.831294186333));
#15462=CARTESIAN_POINT('Ctrl Pts',(0.0915731659545367,12.891080780622,254.636292527683));
#15463=CARTESIAN_POINT('Ctrl Pts',(2.3561195753497,9.02804725529935,254.441290869033));
#15464=CARTESIAN_POINT('Ctrl Pts',(2.53574528220585,4.55379502017353,254.246289210384));
#15465=CARTESIAN_POINT('Ctrl Pts',(0.588162538287489,0.521659120470325,
254.051287551734));
#15466=CARTESIAN_POINT('Ctrl Pts',(-3.02812586089059,-2.11910907686471,
253.856285893084));
#15467=CARTESIAN_POINT('Ctrl Pts',(-7.46176797889057,-2.74681603682514,
253.661284234434));
#15468=CARTESIAN_POINT('Ctrl Pts',(-11.6689892640225,-1.21368606320314,
253.466282575784));
#15469=CARTESIAN_POINT('Ctrl Pts',(-14.6593194902573,2.11934912955326,253.271280917135));
#15470=CARTESIAN_POINT('Ctrl Pts',(-15.7287707153518,6.46762149167933,253.076279258485));
#15471=CARTESIAN_POINT('Ctrl Pts',(-14.625571158157,10.807454345038,252.881277599835));
#15472=CARTESIAN_POINT('Ctrl Pts',(-11.609437681827,14.1171578530651,252.686275941185));
#15473=CARTESIAN_POINT('Ctrl Pts',(-7.39043286771254,15.6175567455485,252.491274282535));
#15474=CARTESIAN_POINT('Ctrl Pts',(-2.96180103757599,14.9554249073266,252.296272623886));
#15475=CARTESIAN_POINT('Ctrl Pts',(0.63386278623459,12.2866423901053,252.101270965236));
#15476=CARTESIAN_POINT('Ctrl Pts',(2.55006213516392,8.23949790130234,251.906269306586));
#15477=CARTESIAN_POINT('Ctrl Pts',(2.33568253872803,3.76677615199603,251.711267647936));
#15478=CARTESIAN_POINT('Ctrl Pts',(0.0411935569874599,-0.0785481218145621,
251.516265989287));
#15479=CARTESIAN_POINT('Ctrl Pts',(-3.79323283755008,-2.39120302105044,
251.321264330637));
#15480=CARTESIAN_POINT('Ctrl Pts',(-8.26489034058072,-2.6267399261753,251.126262671987));
#15481=CARTESIAN_POINT('Ctrl Pts',(-12.3210547625296,-0.729708392383273,
250.931261013337));
#15482=CARTESIAN_POINT('Ctrl Pts',(-15.0068179063841,2.85328962508741,250.736259354687));
#15483=CARTESIAN_POINT('Ctrl Pts',(-15.6898934606167,7.27873946044833,250.541257696038));
#15484=CARTESIAN_POINT('Ctrl Pts',(-14.2094707730794,11.5047952012436,250.346256037388));
#15485=CARTESIAN_POINT('Ctrl Pts',(-10.9140731313682,14.5365525861766,250.151254378738));
#15486=CARTESIAN_POINT('Ctrl Pts',(-6.57950789759873,15.660270830341,249.956252720088));
#15487=CARTESIAN_POINT('Ctrl Pts',(-2.22622479757299,14.6114025311045,249.761251061438));
#15488=CARTESIAN_POINT('Ctrl Pts',(1.12091985526713,11.6368738069172,249.566249402789));
#15489=CARTESIAN_POINT('Ctrl Pts',(2.67393634133375,7.43695258716843,249.371247744139));
#15490=CARTESIAN_POINT('Ctrl Pts',(2.06721123408506,3.00039050572924,249.176246085489));
#15491=CARTESIAN_POINT('Ctrl Pts',(-0.556419348759181,-0.628350463570228,
248.981244426839));
#15492=CARTESIAN_POINT('Ctrl Pts',(-4.57929643494695,-2.59498678201968,
248.786242768189));
#15493=CARTESIAN_POINT('Ctrl Pts',(-9.05434838031283,-2.43653003331118,
248.59124110954));
#15494=CARTESIAN_POINT('Ctrl Pts',(-12.9280518722398,-0.190284338921679,
248.39623945089));
#15495=CARTESIAN_POINT('Ctrl Pts',(-15.2884539309517,3.6149358354734,248.20123779224));
#15496=CARTESIAN_POINT('Ctrl Pts',(-15.5798652377731,8.08329995443233,248.00623613359));
#15497=CARTESIAN_POINT('Ctrl Pts',(-13.7336812979301,12.1628591670547,247.811234474941));
#15498=CARTESIAN_POINT('Ctrl Pts',(-10.184533486267,14.8931976286455,247.616232816291));
#15499=CARTESIAN_POINT('Ctrl Pts',(-5.767967327236,15.6315350660532,247.421231157641));
#15500=CARTESIAN_POINT('Ctrl Pts',(-1.5237374905245,14.2040509382567,247.226229498991));
#15501=CARTESIAN_POINT('Ctrl Pts',(1.54897354961792,10.9468057785166,247.031227840341));
#15502=CARTESIAN_POINT('Ctrl Pts',(2.72678285689953,6.6266247750899,246.836226181692));
#15503=CARTESIAN_POINT('Ctrl Pts',(1.73241052921659,2.26057185924915,246.641224523042));
#15504=CARTESIAN_POINT('Ctrl Pts',(-1.20005053150349,-1.12349160311523,
246.446222864392));
#15505=CARTESIAN_POINT('Ctrl Pts',(-5.38022800707743,-2.72888177693902,
246.251221205742));
#15506=CARTESIAN_POINT('Ctrl Pts',(-9.82403584101992,-2.17766126553081,
246.056219547092));
#15507=CARTESIAN_POINT('Ctrl Pts',(-13.485268418384,0.4004129529351,245.861217888443));
#15508=CARTESIAN_POINT('Ctrl Pts',(-15.5020757887051,4.39837783106898,245.666216229793));
#15509=CARTESIAN_POINT('Ctrl Pts',(-15.3994802353216,8.87508026827576,245.471214571143));
#15510=CARTESIAN_POINT('Ctrl Pts',(-13.2020294654162,12.7764571408952,245.276212912493));
#15511=CARTESIAN_POINT('Ctrl Pts',(-9.42621760171243,15.1842463488826,245.081211253844));
#15512=CARTESIAN_POINT('Ctrl Pts',(-6.45069372495972,15.415165992917,244.951210148077));
#15513=CARTESIAN_POINT('Ctrl Pts',(-5.02255860044595,15.1738049495012,244.886209595194));
#15514=CARTESIAN_POINT('Ctrl Pts',(-1.62711354563937,13.2647104074905,259.432960300116));
#15515=CARTESIAN_POINT('Ctrl Pts',(-0.510856138088382,12.4686551734714,
259.367959747233));
#15516=CARTESIAN_POINT('Ctrl Pts',(1.32296289039781,10.3196571264998,259.237958641467));
#15517=CARTESIAN_POINT('Ctrl Pts',(2.23235101604449,6.17932187292951,259.042956982817));
#15518=CARTESIAN_POINT('Ctrl Pts',(1.08564078396619,2.09885235540685,258.847955324167));
#15519=CARTESIAN_POINT('Ctrl Pts',(-1.84678884916606,-0.96181720811461,
258.652953665517));
#15520=CARTESIAN_POINT('Ctrl Pts',(-5.87474325506511,-2.28177393811631,
258.457952006867));
#15521=CARTESIAN_POINT('Ctrl Pts',(-10.0498725274959,-1.55042684619535,
258.262950348218));
#15522=CARTESIAN_POINT('Ctrl Pts',(-13.3892974790862,1.06012416740417,258.067948689568));
#15523=CARTESIAN_POINT('Ctrl Pts',(-15.1068286426792,4.93526584752227,257.872947030918));
#15524=CARTESIAN_POINT('Ctrl Pts',(-14.7981300152456,9.16272230943613,257.677945372268));
#15525=CARTESIAN_POINT('Ctrl Pts',(-12.5358722883005,12.7472523946929,257.482943713619));
#15526=CARTESIAN_POINT('Ctrl Pts',(-8.8526411453785,14.8449840589292,257.287942054969));
#15527=CARTESIAN_POINT('Ctrl Pts',(-4.61554752403783,14.9620647127609,257.092940396319));
#15528=CARTESIAN_POINT('Ctrl Pts',(-0.82209458746133,13.0709317543718,256.897938737669));
#15529=CARTESIAN_POINT('Ctrl Pts',(1.63465755207235,9.61679816700663,256.702937079019));
#15530=CARTESIAN_POINT('Ctrl Pts',(2.1763366170199,5.41284131032596,256.50793542037));
#15531=CARTESIAN_POINT('Ctrl Pts',(0.675419758711259,1.44876282592323,256.31293376172));
#15532=CARTESIAN_POINT('Ctrl Pts',(-2.51474498300518,-1.34220806487623,
256.11793210307));
#15533=CARTESIAN_POINT('Ctrl Pts',(-6.64312432301459,-2.30301690231008,
255.92293044442));
#15534=CARTESIAN_POINT('Ctrl Pts',(-10.7378091253268,-1.2074686493934,255.72792878577));
#15535=CARTESIAN_POINT('Ctrl Pts',(-13.8348226667817,1.68652110899131,255.532927127121));
#15536=CARTESIAN_POINT('Ctrl Pts',(-15.205061462777,5.69764504670974,255.337925468471));
#15537=CARTESIAN_POINT('Ctrl Pts',(-14.5259418792806,9.88159846318187,255.142923809821));
#15538=CARTESIAN_POINT('Ctrl Pts',(-11.9573432481368,13.2533888885539,254.947922151171));
#15539=CARTESIAN_POINT('Ctrl Pts',(-8.10396883881053,15.0192244590328,254.752920492521));
#15540=CARTESIAN_POINT('Ctrl Pts',(-3.87298572516121,14.763389566186,254.557918833872));
#15541=CARTESIAN_POINT('Ctrl Pts',(-0.260458177839673,12.5461132369294,
254.362917175222));
#15542=CARTESIAN_POINT('Ctrl Pts',(1.88314725198763,8.88938992751473,254.167915516572));
#15543=CARTESIAN_POINT('Ctrl Pts',(2.05317981963823,4.65409082044352,253.972913857922));
#15544=CARTESIAN_POINT('Ctrl Pts',(0.209610207825143,0.837296263906278,
253.777912199273));
#15545=CARTESIAN_POINT('Ctrl Pts',(-3.21354571255632,-1.66243835104231,
253.582910540623));
#15546=CARTESIAN_POINT('Ctrl Pts',(-7.41040353742827,-2.25662182289749,
253.387908881973));
#15547=CARTESIAN_POINT('Ctrl Pts',(-11.392932821826,-0.805370604352179,
253.192907223323));
#15548=CARTESIAN_POINT('Ctrl Pts',(-14.2235606611757,2.34965960715335,252.997905564673));
#15549=CARTESIAN_POINT('Ctrl Pts',(-15.2358964841631,6.46570695648147,252.802903906024));
#15550=CARTESIAN_POINT('Ctrl Pts',(-14.1916147016504,10.5737655197357,252.607902247374));
#15551=CARTESIAN_POINT('Ctrl Pts',(-11.3365616675764,13.706710104793,252.412900588724));
#15552=CARTESIAN_POINT('Ctrl Pts',(-7.34287816854021,15.1269782871939,252.217898930074));
#15553=CARTESIAN_POINT('Ctrl Pts',(-3.15076305073951,14.50020844146,252.022897271425));
#15554=CARTESIAN_POINT('Ctrl Pts',(0.252869775938848,11.9739556469891,251.827895612775));
#15555=CARTESIAN_POINT('Ctrl Pts',(2.06673206286523,8.14295405413105,251.632893954125));
#15556=CARTESIAN_POINT('Ctrl Pts',(1.86380168128525,3.90910369533865,251.437892295475));
#15557=CARTESIAN_POINT('Ctrl Pts',(-0.308147199749915,0.269143852347981,
251.242890636825));
#15558=CARTESIAN_POINT('Ctrl Pts',(-3.93779117856294,-1.92000077226708,
251.047888978175));
#15559=CARTESIAN_POINT('Ctrl Pts',(-8.17063412850482,-2.14295852957143,
250.852887319526));
#15560=CARTESIAN_POINT('Ctrl Pts',(-12.0101739335134,-0.347240376249803,
250.657885660876));
#15561=CARTESIAN_POINT('Ctrl Pts',(-14.5525004826674,3.04440307757636,250.462884002226));
#15562=CARTESIAN_POINT('Ctrl Pts',(-15.1990955186359,7.2335061390772,250.267882343576));
#15563=CARTESIAN_POINT('Ctrl Pts',(-13.7977366865632,11.2338640010921,250.072880684927));
#15564=CARTESIAN_POINT('Ctrl Pts',(-10.6783339448464,14.1037065290698,249.877879026277));
#15565=CARTESIAN_POINT('Ctrl Pts',(-6.57526167726115,15.1674111719922,249.682877367627));
#15566=CARTESIAN_POINT('Ctrl Pts',(-2.45447119486029,14.1745590175435,249.487875708977));
#15567=CARTESIAN_POINT('Ctrl Pts',(0.713914943077987,11.3588887809383,249.292874050327));
#15568=CARTESIAN_POINT('Ctrl Pts',(2.1839906095921,7.38326969265249,249.097872391678));
#15569=CARTESIAN_POINT('Ctrl Pts',(1.60966842793355,3.18364784870049,248.902870733028));
#15570=CARTESIAN_POINT('Ctrl Pts',(-0.873843828610586,-0.251295596465967,
248.707869074378));
#15571=CARTESIAN_POINT('Ctrl Pts',(-4.6818740503375,-2.1129012024424,248.512867415728));
#15572=CARTESIAN_POINT('Ctrl Pts',(-8.91793015810686,-1.96290703782069,
248.317865757078));
#15573=CARTESIAN_POINT('Ctrl Pts',(-12.5847535909962,0.16337504994876,248.122864098429));
#15574=CARTESIAN_POINT('Ctrl Pts',(-14.8190953773418,3.76537260393147,247.927862439779));
#15575=CARTESIAN_POINT('Ctrl Pts',(-15.0949434928954,7.99509805716436,247.732860781129));
#15576=CARTESIAN_POINT('Ctrl Pts',(-13.3473573531331,11.8567832243123,247.537859122479));
#15577=CARTESIAN_POINT('Ctrl Pts',(-9.98775629184481,14.441304489697,247.342857463829));
#15578=CARTESIAN_POINT('Ctrl Pts',(-5.80706246264698,15.1402100777236,247.14785580518));
#15579=CARTESIAN_POINT('Ctrl Pts',(-1.7895011154102,13.7889625543159,246.95285414653));
#15580=CARTESIAN_POINT('Ctrl Pts',(1.11910788576228,10.7056747127731,246.75785248788));
#15581=CARTESIAN_POINT('Ctrl Pts',(2.23401478981833,6.61621846742475,246.56285082923));
#15582=CARTESIAN_POINT('Ctrl Pts',(1.29274818028989,2.48334015745481,246.367849170581));
#15583=CARTESIAN_POINT('Ctrl Pts',(-1.4831010698898,-0.719993094055798,
246.172847511931));
#15584=CARTESIAN_POINT('Ctrl Pts',(-5.44003085375563,-2.23964536495769,
245.977845853281));
#15585=CARTESIAN_POINT('Ctrl Pts',(-9.64651148158805,-1.71786348564419,
245.782844194631));
#15586=CARTESIAN_POINT('Ctrl Pts',(-13.1122112791888,0.722525402070124,
245.587842535981));
#15587=CARTESIAN_POINT('Ctrl Pts',(-15.0213084882368,4.50697388388138,245.392840877332));
#15588=CARTESIAN_POINT('Ctrl Pts',(-14.9241921807959,8.74459233687685,245.197839218682));
#15589=CARTESIAN_POINT('Ctrl Pts',(-12.8440990625429,12.4376112183858,245.002837560032));
#15590=CARTESIAN_POINT('Ctrl Pts',(-9.26993923103672,14.7168093830638,244.807835901382));
#15591=CARTESIAN_POINT('Ctrl Pts',(-6.45332698925382,14.9353964699754,244.677834795616));
#15592=CARTESIAN_POINT('Ctrl Pts',(-5.10146323643611,14.7069256198888,244.612834242732));
#15593=CARTESIAN_POINT('Ctrl Pts',(-1.90203898336826,12.8792000267099,259.159584947655));
#15594=CARTESIAN_POINT('Ctrl Pts',(-0.84876017366957,12.1280577689563,259.094584394772));
#15595=CARTESIAN_POINT('Ctrl Pts',(0.881595844987819,10.1003049498954,258.964583289005));
#15596=CARTESIAN_POINT('Ctrl Pts',(1.73967681811812,6.19356501864459,258.769581630356));
#15597=CARTESIAN_POINT('Ctrl Pts',(0.657663314653353,2.34331323320973,258.574579971706));
#15598=CARTESIAN_POINT('Ctrl Pts',(-2.10932033321967,-0.544675122289394,
258.379578313056));
#15599=CARTESIAN_POINT('Ctrl Pts',(-5.91001987928038,-1.79016065638334,
258.184576654406));
#15600=CARTESIAN_POINT('Ctrl Pts',(-9.849590770955,-1.10007574474532,257.989574995756));
#15601=CARTESIAN_POINT('Ctrl Pts',(-13.00060729662,1.36318948929634,257.794573337106));
#15602=CARTESIAN_POINT('Ctrl Pts',(-14.6212363445191,5.01969791525466,257.599571678457));
#15603=CARTESIAN_POINT('Ctrl Pts',(-14.3299543152493,9.00864372662145,257.404570019807));
#15604=CARTESIAN_POINT('Ctrl Pts',(-12.1953318619067,12.390936695957,257.209568361157));
#15605=CARTESIAN_POINT('Ctrl Pts',(-8.71990649154034,14.3703155519697,257.014566702507));
#15606=CARTESIAN_POINT('Ctrl Pts',(-4.72186724371231,14.4807905829729,256.819565043858));
#15607=CARTESIAN_POINT('Ctrl Pts',(-1.14243872959264,12.6963542532161,256.624563385208));
#15608=CARTESIAN_POINT('Ctrl Pts',(1.17570487397806,9.43710088671688,256.429561726558));
#15609=CARTESIAN_POINT('Ctrl Pts',(1.68682271911594,5.47032884643636,256.234560067908));
#15610=CARTESIAN_POINT('Ctrl Pts',(0.270586722577831,1.72990137929484,256.039558409258));
#15611=CARTESIAN_POINT('Ctrl Pts',(-2.73959076799738,-0.903604546739227,
255.844556750609));
#15612=CARTESIAN_POINT('Ctrl Pts',(-6.63504933142122,-1.81020510481355,
255.649555091959));
#15613=CARTESIAN_POINT('Ctrl Pts',(-10.4987143834928,-0.776467051212444,
255.454553433309));
#15614=CARTESIAN_POINT('Ctrl Pts',(-13.4209962106934,1.954245477432,255.259551774659));
#15615=CARTESIAN_POINT('Ctrl Pts',(-14.7139269256754,5.73906412060058,255.064550116009));
#15616=CARTESIAN_POINT('Ctrl Pts',(-14.0731228766187,9.68696130320919,254.86954845736));
#15617=CARTESIAN_POINT('Ctrl Pts',(-11.6494430958588,12.868517261329,254.67454679871));
#15618=CARTESIAN_POINT('Ctrl Pts',(-8.01347384385351,14.5347254093925,254.47954514006));
#15619=CARTESIAN_POINT('Ctrl Pts',(-4.02120035240413,14.293324573354,254.28454348141));
#15620=CARTESIAN_POINT('Ctrl Pts',(-0.612489521633883,12.2011456932368,
254.089541822761));
#15621=CARTESIAN_POINT('Ctrl Pts',(1.41017492862557,8.75073259973012,253.894540164111));
#15622=CARTESIAN_POINT('Ctrl Pts',(1.57061435707062,4.7543866207135,253.699538505461));
#15623=CARTESIAN_POINT('Ctrl Pts',(-0.168942122637196,1.15293340734223,
253.504536846811));
#15624=CARTESIAN_POINT('Ctrl Pts',(-3.39896556422205,-1.20576762521993,
253.309535188161));
#15625=CARTESIAN_POINT('Ctrl Pts',(-7.35903909596598,-1.76642760896984,
253.114533529512));
#15626=CARTESIAN_POINT('Ctrl Pts',(-11.1168763796294,-0.397055145501226,
252.919531870862));
#15627=CARTESIAN_POINT('Ctrl Pts',(-13.7878018320942,2.57997008475345,252.724530212212));
#15628=CARTESIAN_POINT('Ctrl Pts',(-14.7430222529744,6.46379242128361,252.529528553562));
#15629=CARTESIAN_POINT('Ctrl Pts',(-13.7576582451438,10.3400766944335,252.334526894913));
#15630=CARTESIAN_POINT('Ctrl Pts',(-11.0636856533259,13.2962623565209,252.139525236263));
#15631=CARTESIAN_POINT('Ctrl Pts',(-7.29532346936788,14.6363998288394,251.944523577613));
#15632=CARTESIAN_POINT('Ctrl Pts',(-3.33972506390303,14.0449919755934,251.749521918963));
#15633=CARTESIAN_POINT('Ctrl Pts',(-0.128123234356899,11.6612689038728,
251.554520260313));
#15634=CARTESIAN_POINT('Ctrl Pts',(1.58340199056655,8.04641020695973,251.359518601664));
#15635=CARTESIAN_POINT('Ctrl Pts',(1.39192082384246,4.05143123868129,251.164516943014));
#15636=CARTESIAN_POINT('Ctrl Pts',(-0.657487956487292,0.616835826510511,
250.969515284364));
#15637=CARTESIAN_POINT('Ctrl Pts',(-4.08234951957581,-1.44879852348372,
250.774513625714));
#15638=CARTESIAN_POINT('Ctrl Pts',(-8.07637791642891,-1.65917713296756,
250.579511967064));
#15639=CARTESIAN_POINT('Ctrl Pts',(-11.6992931044972,0.0352276398836714,
250.384510308415));
#15640=CARTESIAN_POINT('Ctrl Pts',(-14.0981830589506,3.23551653006531,250.189508649765));
#15641=CARTESIAN_POINT('Ctrl Pts',(-14.7082975766551,7.18827281770608,249.994506991115));
#15642=CARTESIAN_POINT('Ctrl Pts',(-13.3860026000469,10.9629328009406,249.799505332465));
#15643=CARTESIAN_POINT('Ctrl Pts',(-10.4425947583245,13.670860471963,249.604503673815));
#15644=CARTESIAN_POINT('Ctrl Pts',(-6.57101545692357,14.6745515136434,249.409502015166));
#15645=CARTESIAN_POINT('Ctrl Pts',(-2.68271759214759,13.7377155039824,249.214500356516));
#15646=CARTESIAN_POINT('Ctrl Pts',(0.306910030888837,11.0809037549593,249.019498697866));
#15647=CARTESIAN_POINT('Ctrl Pts',(1.69404487785044,7.32958679813654,248.824497039216));
#15648=CARTESIAN_POINT('Ctrl Pts',(1.15212562178204,3.36690519167174,248.629495380566));
#15649=CARTESIAN_POINT('Ctrl Pts',(-1.19126830846199,0.125759270638291,
248.434493721917));
#15650=CARTESIAN_POINT('Ctrl Pts',(-4.78445166572806,-1.63081562286511,
248.239492063267));
#15651=CARTESIAN_POINT('Ctrl Pts',(-8.78151193590089,-1.48928404233019,
248.044490404617));
#15652=CARTESIAN_POINT('Ctrl Pts',(-12.2414553097526,0.517034438819197,
247.849488745967));
#15653=CARTESIAN_POINT('Ctrl Pts',(-14.3497368237319,3.91580937238954,247.654487087318));
#15654=CARTESIAN_POINT('Ctrl Pts',(-14.6100217480177,7.90689615989639,247.459485428668));
#15655=CARTESIAN_POINT('Ctrl Pts',(-12.9610334083361,11.5507072815698,247.264483770018));
#15656=CARTESIAN_POINT('Ctrl Pts',(-9.79097909742259,13.9894113507484,247.069482111368));
#15657=CARTESIAN_POINT('Ctrl Pts',(-5.84615759805796,14.648885089394,246.874480452718));
#15658=CARTESIAN_POINT('Ctrl Pts',(-2.0552647402959,13.3738741703752,246.679478794069));
#15659=CARTESIAN_POINT('Ctrl Pts',(0.689242221906646,10.4645436470296,246.484477135419));
#15660=CARTESIAN_POINT('Ctrl Pts',(1.74124672273713,6.6058121597596,246.289475476769));
#15661=CARTESIAN_POINT('Ctrl Pts',(0.853085831363201,2.70610845566047,246.094473818119));
#15662=CARTESIAN_POINT('Ctrl Pts',(-1.76615160827613,-0.316494584996361,
245.899472159469));
#15663=CARTESIAN_POINT('Ctrl Pts',(-5.49983370043381,-1.75040895297636,
245.70447050082));
#15664=CARTESIAN_POINT('Ctrl Pts',(-9.46898712215619,-1.25806570575758,
245.50946884217));
#15665=CARTESIAN_POINT('Ctrl Pts',(-12.7391541399936,1.04463785120515,245.31446718352));
#15666=CARTESIAN_POINT('Ctrl Pts',(-14.5405411877685,4.61556993669378,245.11946552487));
#15667=CARTESIAN_POINT('Ctrl Pts',(-14.4489041262702,8.61410440547796,244.924463866221));
#15668=CARTESIAN_POINT('Ctrl Pts',(-12.4861686596696,12.0987652958764,244.729462207571));
#15669=CARTESIAN_POINT('Ctrl Pts',(-9.11366086036101,14.2493724172449,244.534460548921));
#15670=CARTESIAN_POINT('Ctrl Pts',(-6.45596025354793,14.4556269470338,244.404459443155));
#15671=CARTESIAN_POINT('Ctrl Pts',(-5.18036787242628,14.2400462902765,244.339458890271));
#15672=CARTESIAN_POINT('Ctrl Pts',(-2.17696442109716,12.4936896459294,258.886209595194));
#15673=CARTESIAN_POINT('Ctrl Pts',(-1.18666420925076,11.7874603644412,258.82120904231));
#15674=CARTESIAN_POINT('Ctrl Pts',(0.440228799577828,9.88095277329113,258.691207936544));
#15675=CARTESIAN_POINT('Ctrl Pts',(1.24700262019175,6.20780816435965,258.496206277894));
#15676=CARTESIAN_POINT('Ctrl Pts',(0.229685845340515,2.58777411101262,258.301204619244));
#15677=CARTESIAN_POINT('Ctrl Pts',(-2.37185181727327,-0.127533036464177,
258.106202960595));
#15678=CARTESIAN_POINT('Ctrl Pts',(-5.94529650349566,-1.29854737465037,
257.911201301945));
#15679=CARTESIAN_POINT('Ctrl Pts',(-9.64930901441413,-0.649724643295287,
257.716199643295));
#15680=CARTESIAN_POINT('Ctrl Pts',(-12.6119171141539,1.66625481118851,257.521197984645));
#15681=CARTESIAN_POINT('Ctrl Pts',(-14.135644046359,5.10412998298705,257.326196325996));
#15682=CARTESIAN_POINT('Ctrl Pts',(-13.861778615253,8.85456514380678,257.131194667346));
#15683=CARTESIAN_POINT('Ctrl Pts',(-11.8547914355129,12.034620997221,256.936193008696));
#15684=CARTESIAN_POINT('Ctrl Pts',(-8.58717183770218,13.8956470450103,256.741191350046));
#15685=CARTESIAN_POINT('Ctrl Pts',(-4.82818696338679,13.9995164531848,256.546189691396));
#15686=CARTESIAN_POINT('Ctrl Pts',(-1.46278287172395,12.3217767520604,256.351188032747));
#15687=CARTESIAN_POINT('Ctrl Pts',(0.716752195883785,9.25740360642712,256.156186374097));
#15688=CARTESIAN_POINT('Ctrl Pts',(1.19730882121199,5.52781638254676,255.961184715447));
#15689=CARTESIAN_POINT('Ctrl Pts',(-0.134246313555596,2.01103993266644,
255.766183056797));
#15690=CARTESIAN_POINT('Ctrl Pts',(-2.96443655298958,-0.465001028602228,
255.571181398147));
#15691=CARTESIAN_POINT('Ctrl Pts',(-6.62697433982785,-1.31739330731701,
255.376179739498));
#15692=CARTESIAN_POINT('Ctrl Pts',(-10.2596196416587,-0.345465453031489,
255.181178080848));
#15693=CARTESIAN_POINT('Ctrl Pts',(-13.0071697546051,2.22196984587269,254.986176422198));
#15694=CARTESIAN_POINT('Ctrl Pts',(-14.2227923885739,5.78048319449142,254.791174763548));
#15695=CARTESIAN_POINT('Ctrl Pts',(-13.6203038739569,9.4923241432365,254.596173104898));
#15696=CARTESIAN_POINT('Ctrl Pts',(-11.3415429435809,12.4836456341042,254.401171446249));
#15697=CARTESIAN_POINT('Ctrl Pts',(-7.92297884889648,14.0502263597522,254.206169787599));
#15698=CARTESIAN_POINT('Ctrl Pts',(-4.16941497964704,13.8232595805219,254.011168128949));
#15699=CARTESIAN_POINT('Ctrl Pts',(-0.964520865428091,11.8561781495442,
253.816166470299));
#15700=CARTESIAN_POINT('Ctrl Pts',(0.937202605263502,8.61207527194551,253.62116481165));
#15701=CARTESIAN_POINT('Ctrl Pts',(1.088048894503,4.85468242098349,253.426163153));
#15702=CARTESIAN_POINT('Ctrl Pts',(-0.547494453099542,1.46857055077819,
253.23116149435));
#15703=CARTESIAN_POINT('Ctrl Pts',(-3.58438541588777,-0.749096899397535,
253.0361598357));
#15704=CARTESIAN_POINT('Ctrl Pts',(-7.3076746545037,-1.27623339504218,252.84115817705));
#15705=CARTESIAN_POINT('Ctrl Pts',(-10.8408199374328,0.0112603133497307,
252.646156518401));
#15706=CARTESIAN_POINT('Ctrl Pts',(-13.3520430030127,2.81028056235354,252.451154859751));
#15707=CARTESIAN_POINT('Ctrl Pts',(-14.2501480217857,6.46187788608574,252.256153201101));
#15708=CARTESIAN_POINT('Ctrl Pts',(-13.3237017886373,10.1063878691313,252.061151542451));
#15709=CARTESIAN_POINT('Ctrl Pts',(-10.7908096390754,12.8858146082488,251.866149883801));
#15710=CARTESIAN_POINT('Ctrl Pts',(-7.24776877019554,14.1458213704849,251.671148225152));
#15711=CARTESIAN_POINT('Ctrl Pts',(-3.52868707706655,13.5897755097268,251.476146566502));
#15712=CARTESIAN_POINT('Ctrl Pts',(-0.509116244652642,11.3485821607565,
251.281144907852));
#15713=CARTESIAN_POINT('Ctrl Pts',(1.10007191826787,7.94986635978842,251.086143249202));
#15714=CARTESIAN_POINT('Ctrl Pts',(0.920039966399679,4.19375878202392,250.891141590553));
#15715=CARTESIAN_POINT('Ctrl Pts',(-1.00682871322467,0.964527800673052,
250.696139931903));
#15716=CARTESIAN_POINT('Ctrl Pts',(-4.22690786058867,-0.977596274700365,
250.501138273253));
#15717=CARTESIAN_POINT('Ctrl Pts',(-7.98212170435301,-1.1753957363637,250.306136614603));
#15718=CARTESIAN_POINT('Ctrl Pts',(-11.388412275481,0.417695656017143,250.111134955953));
#15719=CARTESIAN_POINT('Ctrl Pts',(-13.6438656352338,3.42662998255425,249.916133297304));
#15720=CARTESIAN_POINT('Ctrl Pts',(-14.2174996346742,7.14303949633495,249.721131638654));
#15721=CARTESIAN_POINT('Ctrl Pts',(-12.9742685135307,10.6920016007892,249.526129980004));
#15722=CARTESIAN_POINT('Ctrl Pts',(-10.2068555718026,13.2380144148563,249.331128321354));
#15723=CARTESIAN_POINT('Ctrl Pts',(-6.56676923658599,14.1816918552946,249.136126662704));
#15724=CARTESIAN_POINT('Ctrl Pts',(-2.91096398943488,13.3008719904214,248.941125004055));
#15725=CARTESIAN_POINT('Ctrl Pts',(-0.100094881300308,10.8029187289803,
248.746123345405));
#15726=CARTESIAN_POINT('Ctrl Pts',(1.20409914610878,7.27590390362059,248.551121686755));
#15727=CARTESIAN_POINT('Ctrl Pts',(0.69458281563053,3.55016253464298,248.356120028105));
#15728=CARTESIAN_POINT('Ctrl Pts',(-1.50869278831339,0.502814137742552,
248.161118369455));
#15729=CARTESIAN_POINT('Ctrl Pts',(-4.88702928111861,-1.14873004328783,
247.966116710806));
#15730=CARTESIAN_POINT('Ctrl Pts',(-8.64509371369493,-1.0156610468397,247.771115052156));
#15731=CARTESIAN_POINT('Ctrl Pts',(-11.898157028509,0.870693827689635,247.576113393506));
#15732=CARTESIAN_POINT('Ctrl Pts',(-13.880378270122,4.06624614084761,247.381111734856));
#15733=CARTESIAN_POINT('Ctrl Pts',(-14.12510000314,7.81869426262842,247.186110076207));
#15734=CARTESIAN_POINT('Ctrl Pts',(-12.5747094635392,11.2446313388274,246.991108417557));
#15735=CARTESIAN_POINT('Ctrl Pts',(-9.59420190300037,13.5375182117999,246.796106758907));
#15736=CARTESIAN_POINT('Ctrl Pts',(-5.88525273346894,14.1575601010644,246.601105100257));
#15737=CARTESIAN_POINT('Ctrl Pts',(-2.3210283651816,12.9587857864344,246.406103441607));
#15738=CARTESIAN_POINT('Ctrl Pts',(0.259376558051009,10.2234125812861,246.211101782958));
#15739=CARTESIAN_POINT('Ctrl Pts',(1.24847865565592,6.59540585209445,246.016100124308));
#15740=CARTESIAN_POINT('Ctrl Pts',(0.413423482436507,2.92887675386613,245.821098465658));
#15741=CARTESIAN_POINT('Ctrl Pts',(-2.04920214666245,0.0870039240630693,
245.626096807008));
#15742=CARTESIAN_POINT('Ctrl Pts',(-5.55963654711201,-1.26117254099502,
245.431095148358));
#15743=CARTESIAN_POINT('Ctrl Pts',(-9.29146276272433,-0.798267925870965,
245.236093489709));
#15744=CARTESIAN_POINT('Ctrl Pts',(-12.3660970007984,1.36675030034017,245.041091831059));
#15745=CARTESIAN_POINT('Ctrl Pts',(-14.0597738873002,4.72416598950618,244.846090172409));
#15746=CARTESIAN_POINT('Ctrl Pts',(-13.9736160717445,8.48361647407905,244.651088513759));
#15747=CARTESIAN_POINT('Ctrl Pts',(-12.1282382567964,11.7599193733671,244.45608685511));
#15748=CARTESIAN_POINT('Ctrl Pts',(-8.95738248968529,13.781935451426,244.26108519646));
#15749=CARTESIAN_POINT('Ctrl Pts',(-6.45859351784204,13.9758574240922,244.131084090693));
#15750=CARTESIAN_POINT('Ctrl Pts',(-5.25927250841645,13.7731669606642,244.06608353781));
#15751=CARTESIAN_POINT('',(-5.02255860044588,15.1738049495011,244.886209595194));
#15752=CARTESIAN_POINT('Ctrl Pts',(-13.5606802741686,4.06871967504047,244.886209595194));
#15753=CARTESIAN_POINT('Ctrl Pts',(-13.6416999058547,4.25198474135208,244.886209595194));
#15754=CARTESIAN_POINT('Ctrl Pts',(-13.7151826312799,4.43828315373224,244.886209595194));
#15755=CARTESIAN_POINT('Ctrl Pts',(-13.7809288919042,4.62715219586253,244.886209595194));
#15756=CARTESIAN_POINT('Ctrl Pts',(-13.7981238459847,4.67654807748114,244.886209595194));
#15757=CARTESIAN_POINT('Ctrl Pts',(-13.8147894265217,4.72611998925969,244.886209595194));
#15758=CARTESIAN_POINT('Ctrl Pts',(-13.8309216335706,4.77586005181989,244.886209595194));
#15759=CARTESIAN_POINT('Ctrl Pts',(-13.8920913619837,4.96446326704244,244.886209595194));
#15760=CARTESIAN_POINT('Ctrl Pts',(-13.9455960634865,5.15548198727219,244.886209595194));
#15761=CARTESIAN_POINT('Ctrl Pts',(-13.9914834408764,5.34843841990208,244.886209595194));
#15762=CARTESIAN_POINT('Ctrl Pts',(-14.0221712830238,5.47748080329141,244.886209595194));
#15763=CARTESIAN_POINT('Ctrl Pts',(-14.0494513794723,5.60739045083055,244.886209595194));
#15764=CARTESIAN_POINT('Ctrl Pts',(-14.0733263319475,5.73803005416043,244.886209595194));
#15765=CARTESIAN_POINT('Ctrl Pts',(-14.0848264366772,5.80095663471375,244.886209595194));
#15766=CARTESIAN_POINT('Ctrl Pts',(-14.0955363513703,5.86405263259847,244.886209595194));
#15767=CARTESIAN_POINT('Ctrl Pts',(-14.1054555711143,5.92730296672008,244.886209595194));
#15768=CARTESIAN_POINT('Ctrl Pts',(-14.1099102436318,5.95570837887997,244.886209595194));
#15769=CARTESIAN_POINT('Ctrl Pts',(-14.114203857297,5.98413486412789,244.886209595194));
#15770=CARTESIAN_POINT('Ctrl Pts',(-14.1183365861332,6.01258036983195,244.886209595194));
#15771=CARTESIAN_POINT('Ctrl Pts',(-14.148435975581,6.21975398033503,244.886209595194));
#15772=CARTESIAN_POINT('Ctrl Pts',(-14.1700072218867,6.42794420942989,244.886209595194));
#15773=CARTESIAN_POINT('Ctrl Pts',(-14.183122304898,6.63659797625938,244.886209595194));
#15774=CARTESIAN_POINT('Ctrl Pts',(-14.1959167986966,6.84015134480945,244.886209595194));
#15775=CARTESIAN_POINT('Ctrl Pts',(-14.200663401768,7.04414668470632,244.886209595194));
#15776=CARTESIAN_POINT('Ctrl Pts',(-14.1973790954965,7.24809133966967,244.886209595194));
#15777=CARTESIAN_POINT('Ctrl Pts',(-14.1939713478628,7.45970129863671,244.886209595194));
#15778=CARTESIAN_POINT('Ctrl Pts',(-14.1819181544029,7.67125743925327,244.886209595194));
#15779=CARTESIAN_POINT('Ctrl Pts',(-14.1611803257851,7.88222052991278,244.886209595194));
#15780=CARTESIAN_POINT('Ctrl Pts',(-14.1585245428646,7.90923744587584,244.886209595194));
#15781=CARTESIAN_POINT('Ctrl Pts',(-14.1557261469623,7.93624508772895,244.886209595194));
#15782=CARTESIAN_POINT('Ctrl Pts',(-14.1527868126277,7.96322691161578,244.886209595194));
#15783=CARTESIAN_POINT('Ctrl Pts',(-14.1327741913593,8.14693415995982,244.886209595194));
#15784=CARTESIAN_POINT('Ctrl Pts',(-14.1062143898519,8.32961625926344,244.886209595194));
#15785=CARTESIAN_POINT('Ctrl Pts',(-14.0731550923849,8.51091582075917,244.886209595194));
#15786=CARTESIAN_POINT('Ctrl Pts',(-14.0365821385092,8.71148452633737,244.886209595194));
#15787=CARTESIAN_POINT('Ctrl Pts',(-13.9920559713202,8.91036170495516,244.886209595194));
#15788=CARTESIAN_POINT('Ctrl Pts',(-13.9398818306279,9.10715451221913,244.886209595194));
#15789=CARTESIAN_POINT('Ctrl Pts',(-13.8870437200209,9.30645171153857,244.886209595194));
#15790=CARTESIAN_POINT('Ctrl Pts',(-13.8263616491073,9.5036117606046,244.886209595194));
#15791=CARTESIAN_POINT('Ctrl Pts',(-13.7580989406148,9.69822902231716,244.886209595194));
#15792=CARTESIAN_POINT('Ctrl Pts',(-13.6893937488177,9.8941078057447,244.886209595194));
#15793=CARTESIAN_POINT('Ctrl Pts',(-13.613009170321,10.0874113903711,244.886209595194));
#15794=CARTESIAN_POINT('Ctrl Pts',(-13.5291615501821,10.2777189855474,244.886209595194));
#15795=CARTESIAN_POINT('Ctrl Pts',(-13.4588847736849,10.4372250551266,244.886209595194));
#15796=CARTESIAN_POINT('Ctrl Pts',(-13.3833642870213,10.5946265393459,244.886209595194));
#15797=CARTESIAN_POINT('Ctrl Pts',(-13.3027008011542,10.7496666223443,244.886209595194));
#15798=CARTESIAN_POINT('Ctrl Pts',(-13.2894851256601,10.7750679474108,244.886209595194));
#15799=CARTESIAN_POINT('Ctrl Pts',(-13.2761313475271,10.8004058623963,244.886209595194));
#15800=CARTESIAN_POINT('Ctrl Pts',(-13.2626398501178,10.8256792079891,244.886209595194));
#15801=CARTESIAN_POINT('Ctrl Pts',(-13.2511902780452,10.847127456697,244.886209595194));
#15802=CARTESIAN_POINT('Ctrl Pts',(-13.2396441383265,10.8685242469617,244.886209595194));
#15803=CARTESIAN_POINT('Ctrl Pts',(-13.228005484279,10.8898623047447,244.886209595194));
#15804=CARTESIAN_POINT('Ctrl Pts',(-13.1266071084601,11.0757639041474,244.886209595194));
#15805=CARTESIAN_POINT('Ctrl Pts',(-13.0181082120307,11.2573630403096,244.886209595194));
#15806=CARTESIAN_POINT('Ctrl Pts',(-12.9028146193286,11.4342494127783,244.886209595194));
#15807=CARTESIAN_POINT('Ctrl Pts',(-12.7863855232406,11.6128779035223,244.886209595194));
#15808=CARTESIAN_POINT('Ctrl Pts',(-12.6630270719645,11.7867010213949,244.886209595194));
#15809=CARTESIAN_POINT('Ctrl Pts',(-12.5330020233028,11.9552883416326,244.886209595194));
#15810=CARTESIAN_POINT('Ctrl Pts',(-12.5051012498885,11.9914638068286,244.886209595194));
#15811=CARTESIAN_POINT('Ctrl Pts',(-12.4768933316999,12.0273981416757,244.886209595194));
#15812=CARTESIAN_POINT('Ctrl Pts',(-12.4483805671437,12.063086999528,244.886209595194));
#15813=CARTESIAN_POINT('Ctrl Pts',(-12.3164995738421,12.2281598045195,244.886209595194));
#15814=CARTESIAN_POINT('Ctrl Pts',(-12.1781005112301,12.3879829814049,244.886209595194));
#15815=CARTESIAN_POINT('Ctrl Pts',(-12.033606732815,12.5423224318724,244.886209595194));
#15816=CARTESIAN_POINT('Ctrl Pts',(-11.8882086532915,12.6976278016873,244.886209595194));
#15817=CARTESIAN_POINT('Ctrl Pts',(-11.7366388964776,12.8473810885217,244.886209595194));
#15818=CARTESIAN_POINT('Ctrl Pts',(-11.5792852838968,12.9913137785295,244.886209595194));
#15819=CARTESIAN_POINT('Ctrl Pts',(-11.4919827660588,13.071170135373,244.886209595194));
#15820=CARTESIAN_POINT('Ctrl Pts',(-11.4028991143817,13.1492342086978,244.886209595194));
#15821=CARTESIAN_POINT('Ctrl Pts',(-11.3120956067516,13.2254553247554,244.886209595194));
#15822=CARTESIAN_POINT('Ctrl Pts',(-11.2929324571765,13.2415410100545,244.886209595194));
#15823=CARTESIAN_POINT('Ctrl Pts',(-11.2736926976274,13.2575446008321,244.886209595194));
#15824=CARTESIAN_POINT('Ctrl Pts',(-11.2543768861651,13.273465599029,244.886209595194));
#15825=CARTESIAN_POINT('Ctrl Pts',(-11.2343851389903,13.2899437351582,244.886209595194));
#15826=CARTESIAN_POINT('Ctrl Pts',(-11.214318599184,13.3063278760051,244.886209595194));
#15827=CARTESIAN_POINT('Ctrl Pts',(-11.1941818061718,13.3226146508888,244.886209595194));
#15828=CARTESIAN_POINT('Ctrl Pts',(-11.0256711873371,13.4589071833097,244.886209595194));
#15829=CARTESIAN_POINT('Ctrl Pts',(-10.85216239996,13.5884512574688,244.886209595194));
#15830=CARTESIAN_POINT('Ctrl Pts',(-10.6741349526739,13.7110348714328,244.886209595194));
#15831=CARTESIAN_POINT('Ctrl Pts',(-10.4945591404068,13.8346846365887,244.886209595194));
#15832=CARTESIAN_POINT('Ctrl Pts',(-10.3103852764165,13.9512528349893,244.886209595194));
#15833=CARTESIAN_POINT('Ctrl Pts',(-10.1220600987603,14.0604937305074,244.886209595194));
#15834=CARTESIAN_POINT('Ctrl Pts',(-9.9332803739495,14.1699982930447,244.886209595194));
#15835=CARTESIAN_POINT('Ctrl Pts',(-9.74032876130808,14.2721406262152,244.886209595194));
#15836=CARTESIAN_POINT('Ctrl Pts',(-9.54361713581158,14.3666376844702,244.886209595194));
#15837=CARTESIAN_POINT('Ctrl Pts',(-9.43177984793535,14.4203624944851,244.886209595194));
#15838=CARTESIAN_POINT('Ctrl Pts',(-9.31872655436916,14.4716154268187,244.886209595194));
#15839=CARTESIAN_POINT('Ctrl Pts',(-9.20452844087298,14.5203384387715,244.886209595194));
#15840=CARTESIAN_POINT('Ctrl Pts',(-9.04092708943691,14.5901395095377,244.886209595194));
#15841=CARTESIAN_POINT('Ctrl Pts',(-8.87497648096828,14.6547491997806,244.886209595194));
#15842=CARTESIAN_POINT('Ctrl Pts',(-8.70692766233866,14.7141407892771,244.886209595194));
#15843=CARTESIAN_POINT('Ctrl Pts',(-8.6334063041882,14.7401246096819,244.886209595194));
#15844=CARTESIAN_POINT('Ctrl Pts',(-8.55948320988161,14.7651093791428,244.886209595194));
#15845=CARTESIAN_POINT('Ctrl Pts',(-8.48517889259629,14.7890915593904,244.886209595194));
#15846=CARTESIAN_POINT('Ctrl Pts',(-8.44998101678734,14.8004518925826,244.886209595194));
#15847=CARTESIAN_POINT('Ctrl Pts',(-8.41469759425489,14.8115872424219,244.886209595194));
#15848=CARTESIAN_POINT('Ctrl Pts',(-8.37933078649837,14.8224971691949,244.886209595194));
#15849=CARTESIAN_POINT('Ctrl Pts',(-8.35485045205377,14.8300488447097,244.886209595194));
#15850=CARTESIAN_POINT('Ctrl Pts',(-8.33033806182638,14.8374900653625,244.886209595194));
#15851=CARTESIAN_POINT('Ctrl Pts',(-8.30579869883627,14.8448196425142,244.886209595194));
#15852=CARTESIAN_POINT('Ctrl Pts',(-8.09581085169372,14.9075401836779,244.886209595194));
#15853=CARTESIAN_POINT('Ctrl Pts',(-7.88375132882739,14.9621196129436,244.886209595194));
#15854=CARTESIAN_POINT('Ctrl Pts',(-7.67013298256505,15.0086098677565,244.886209595194));
#15855=CARTESIAN_POINT('Ctrl Pts',(-7.45228817486406,15.0560199371483,244.886209595194));
#15856=CARTESIAN_POINT('Ctrl Pts',(-7.23282171750465,15.0950178682759,244.886209595194));
#15857=CARTESIAN_POINT('Ctrl Pts',(-7.0122464777467,15.125614080605,244.886209595194));
#15858=CARTESIAN_POINT('Ctrl Pts',(-6.79076187738696,15.1563364312535,244.886209595194));
#15859=CARTESIAN_POINT('Ctrl Pts',(-6.56815868414206,15.1785878405488,244.886209595194));
#15860=CARTESIAN_POINT('Ctrl Pts',(-6.34493423868892,15.1923307336774,244.886209595194));
#15861=CARTESIAN_POINT('Ctrl Pts',(-6.12307246678007,15.20598973332,244.886209595194));
#15862=CARTESIAN_POINT('Ctrl Pts',(-5.90059633001586,15.2112438988409,244.886209595194));
#15863=CARTESIAN_POINT('Ctrl Pts',(-5.67798247999417,15.208006677574,244.886209595194));
#15864=CARTESIAN_POINT('Ctrl Pts',(-5.45949145586512,15.2048294098979,244.886209595194));
#15865=CARTESIAN_POINT('Ctrl Pts',(-5.24086713902449,15.1934723799368,244.886209595194));
#15866=CARTESIAN_POINT('Ctrl Pts',(-5.02255860044619,15.1738049495012,244.886209595194));
#15867=CARTESIAN_POINT('Ctrl Pts',(-2.5565939916359,-1.50913350781789,258.886209595194));
#15868=CARTESIAN_POINT('Ctrl Pts',(-2.36425176395604,-1.3944894355529,258.886209595194));
#15869=CARTESIAN_POINT('Ctrl Pts',(-2.1766718434797,-1.27277478699839,258.886209595194));
#15870=CARTESIAN_POINT('Ctrl Pts',(-1.99428412292338,-1.14416896494428,
258.886209595194));
#15871=CARTESIAN_POINT('Ctrl Pts',(-1.93366427166563,-1.10142449848557,
258.886209595194));
#15872=CARTESIAN_POINT('Ctrl Pts',(-1.87361822779059,-1.0579184173449,258.886209595194));
#15873=CARTESIAN_POINT('Ctrl Pts',(-1.81416252640475,-1.01365627442405,
258.886209595194));
#15874=CARTESIAN_POINT('Ctrl Pts',(-1.63480680238428,-0.88013386185092,
258.886209595194));
#15875=CARTESIAN_POINT('Ctrl Pts',(-1.4608203694423,-0.739733919894315,
258.886209595194));
#15876=CARTESIAN_POINT('Ctrl Pts',(-1.29251314946164,-0.592851231854552,
258.886209595194));
#15877=CARTESIAN_POINT('Ctrl Pts',(-1.12422973111361,-0.445989315637765,
258.886209595194));
#15878=CARTESIAN_POINT('Ctrl Pts',(-0.961623522417777,-0.29264590162531,
258.886209595194));
#15879=CARTESIAN_POINT('Ctrl Pts',(-0.805045885791296,-0.133184447506872,
258.886209595194));
#15880=CARTESIAN_POINT('Ctrl Pts',(-0.649718484741496,0.0250037444309419,
258.886209595194));
#15881=CARTESIAN_POINT('Ctrl Pts',(-0.500323440890837,0.189213250571515,
258.886209595194));
#15882=CARTESIAN_POINT('Ctrl Pts',(-0.357249980777704,0.359111132088609,
258.886209595194));
#15883=CARTESIAN_POINT('Ctrl Pts',(-0.29718860122125,0.430433242699247,
258.886209595194));
#15884=CARTESIAN_POINT('Ctrl Pts',(-0.238241845667419,0.50275801433704,
258.886209595194));
#15885=CARTESIAN_POINT('Ctrl Pts',(-0.180441176696654,0.576061603721381,
258.886209595194));
#15886=CARTESIAN_POINT('Ctrl Pts',(-0.144784954550875,0.621281306429199,
258.886209595194));
#15887=CARTESIAN_POINT('Ctrl Pts',(-0.109564900728486,0.666873500247899,
258.886209595194));
#15888=CARTESIAN_POINT('Ctrl Pts',(-0.0747887191667214,0.712832650035259,
258.886209595194));
#15889=CARTESIAN_POINT('Ctrl Pts',(-0.0563480485347127,0.73720328262615,
258.886209595194));
#15890=CARTESIAN_POINT('Ctrl Pts',(-0.038030742298959,0.761679150596887,
258.886209595194));
#15891=CARTESIAN_POINT('Ctrl Pts',(-0.0198518056549546,0.78624046597595,
258.886209595194));
#15892=CARTESIAN_POINT('Ctrl Pts',(0.110489913750218,0.9623433998302,258.886209595194));
#15893=CARTESIAN_POINT('Ctrl Pts',(0.233876948226976,1.14303894425533,258.886209595194));
#15894=CARTESIAN_POINT('Ctrl Pts',(0.35002118159745,1.32795518664564,258.886209595194));
#15895=CARTESIAN_POINT('Ctrl Pts',(0.465425226174361,1.51169295528488,258.886209595194));
#15896=CARTESIAN_POINT('Ctrl Pts',(0.573678798737716,1.69959838513866,258.886209595194));
#15897=CARTESIAN_POINT('Ctrl Pts',(0.674454146436358,1.89133064568259,258.886209595194));
#15898=CARTESIAN_POINT('Ctrl Pts',(0.734138634723959,2.00488462609662,258.886209595194));
#15899=CARTESIAN_POINT('Ctrl Pts',(0.791199155867516,2.11978133151867,258.886209595194));
#15900=CARTESIAN_POINT('Ctrl Pts',(0.84555942095047,2.23595271429465,258.886209595194));
#15901=CARTESIAN_POINT('Ctrl Pts',(0.937957038195646,2.43341236509285,258.886209595194));
#15902=CARTESIAN_POINT('Ctrl Pts',(1.02255618128302,2.63455462652551,258.886209595194));
#15903=CARTESIAN_POINT('Ctrl Pts',(1.09921502593214,2.83889578394013,258.886209595194));
#15904=CARTESIAN_POINT('Ctrl Pts',(1.17522871899264,3.04151723082521,258.886209595194));
#15905=CARTESIAN_POINT('Ctrl Pts',(1.24343521127095,3.24728464096187,258.886209595194));
#15906=CARTESIAN_POINT('Ctrl Pts',(1.30364535510154,3.45572494737603,258.886209595194));
#15907=CARTESIAN_POINT('Ctrl Pts',(1.32167511638107,3.51814182145381,258.886209595194));
#15908=CARTESIAN_POINT('Ctrl Pts',(1.33898750665215,3.58079832257484,258.886209595194));
#15909=CARTESIAN_POINT('Ctrl Pts',(1.35557654598764,3.64368158286573,258.886209595194));
#15910=CARTESIAN_POINT('Ctrl Pts',(1.36363610324781,3.67423255250119,258.886209595194));
#15911=CARTESIAN_POINT('Ctrl Pts',(1.37152572241146,3.70484048731049,258.886209595194));
#15912=CARTESIAN_POINT('Ctrl Pts',(1.37923843311511,3.73547835131255,258.886209595194));
#15913=CARTESIAN_POINT('Ctrl Pts',(1.43147363965295,3.94297675434062,258.886209595194));
#15914=CARTESIAN_POINT('Ctrl Pts',(1.47566023134054,4.15207335701424,258.886209595194));
#15915=CARTESIAN_POINT('Ctrl Pts',(1.51173350642158,4.36229864068028,258.886209595194));
#15916=CARTESIAN_POINT('Ctrl Pts',(1.54773548735025,4.57210844132261,258.886209595194));
#15917=CARTESIAN_POINT('Ctrl Pts',(1.57565622252453,4.78304316299326,258.886209595194));
#15918=CARTESIAN_POINT('Ctrl Pts',(1.59537984651403,4.99464074758762,258.886209595194));
#15919=CARTESIAN_POINT('Ctrl Pts',(1.6148216062332,5.20321445589954,258.886209595194));
#15920=CARTESIAN_POINT('Ctrl Pts',(1.62629879805449,5.41243284840401,258.886209595194));
#15921=CARTESIAN_POINT('Ctrl Pts',(1.62965074073741,5.62184810818147,258.886209595194));
#15922=CARTESIAN_POINT('Ctrl Pts',(1.6327194156952,5.8135659936726,258.886209595194));
#15923=CARTESIAN_POINT('Ctrl Pts',(1.62897759367094,6.00544917304189,258.886209595194));
#15924=CARTESIAN_POINT('Ctrl Pts',(1.61826513272597,6.19714342809054,258.886209595194));
#15925=CARTESIAN_POINT('Ctrl Pts',(1.60917103257037,6.35987790746193,258.886209595194));
#15926=CARTESIAN_POINT('Ctrl Pts',(1.59505249145376,6.5224762007389,258.886209595194));
#15927=CARTESIAN_POINT('Ctrl Pts',(1.57593654055478,6.68470751761093,258.886209595194));
#15928=CARTESIAN_POINT('Ctrl Pts',(1.5719647517677,6.71841489260214,258.886209595194));
#15929=CARTESIAN_POINT('Ctrl Pts',(1.56777717341846,6.75210639050512,258.886209595194));
#15930=CARTESIAN_POINT('Ctrl Pts',(1.56337396690442,6.78577988384794,258.886209595194));
#15931=CARTESIAN_POINT('Ctrl Pts',(1.5587180818881,6.82138573440307,258.886209595194));
#15932=CARTESIAN_POINT('Ctrl Pts',(1.55382011111554,6.85697788318115,258.886209595194));
#15933=CARTESIAN_POINT('Ctrl Pts',(1.54868546689053,6.89251890151437,258.886209595194));
#15934=CARTESIAN_POINT('Ctrl Pts',(1.51896610042817,7.09823063187067,258.886209595194));
#15935=CARTESIAN_POINT('Ctrl Pts',(1.48130244852888,7.30240357228093,258.886209595194));
#15936=CARTESIAN_POINT('Ctrl Pts',(1.43587337478814,7.50459721844464,258.886209595194));
#15937=CARTESIAN_POINT('Ctrl Pts',(1.38852851662937,7.71531755038135,258.886209595194));
#15938=CARTESIAN_POINT('Ctrl Pts',(1.33274952436721,7.92388900443129,258.886209595194));
#15939=CARTESIAN_POINT('Ctrl Pts',(1.26868210430257,8.12979485754507,258.886209595194));
#15940=CARTESIAN_POINT('Ctrl Pts',(1.20747747983608,8.3264999910211,258.886209595194));
#15941=CARTESIAN_POINT('Ctrl Pts',(1.13870795870331,8.5207728894651,258.886209595194));
#15942=CARTESIAN_POINT('Ctrl Pts',(1.06245554283562,8.71213744821539,258.886209595194));
#15943=CARTESIAN_POINT('Ctrl Pts',(0.987089797793576,8.9012768004673,258.886209595194));
#15944=CARTESIAN_POINT('Ctrl Pts',(0.904413843326177,9.08757558348147,258.886209595194));
#15945=CARTESIAN_POINT('Ctrl Pts',(0.814468490237699,9.2705410852132,258.886209595194));
#15946=CARTESIAN_POINT('Ctrl Pts',(0.762052691576746,9.3771645245724,258.886209595194));
#15947=CARTESIAN_POINT('Ctrl Pts',(0.707167515950218,9.4826553245914,258.886209595194));
#15948=CARTESIAN_POINT('Ctrl Pts',(0.649815571343313,9.58690963773167,258.886209595194));
#15949=CARTESIAN_POINT('Ctrl Pts',(0.628692976237029,9.6253062720505,258.886209595194));
#15950=CARTESIAN_POINT('Ctrl Pts',(0.607235742908852,9.66353513548064,258.886209595194));
#15951=CARTESIAN_POINT('Ctrl Pts',(0.585443872533378,9.70159086009454,258.886209595194));
#15952=CARTESIAN_POINT('Ctrl Pts',(0.569448520810109,9.72952396954294,258.886209595194));
#15953=CARTESIAN_POINT('Ctrl Pts',(0.55327160296368,9.75736582506558,258.886209595194));
#15954=CARTESIAN_POINT('Ctrl Pts',(0.536925022550999,9.78509443608612,258.886209595194));
#15955=CARTESIAN_POINT('Ctrl Pts',(0.515073579604955,9.82216091399109,258.886209595194));
#15956=CARTESIAN_POINT('Ctrl Pts',(0.492914635658092,9.85903272341201,258.886209595194));
#15957=CARTESIAN_POINT('Ctrl Pts',(0.470449172522589,9.89570560295486,258.886209595194));
#15958=CARTESIAN_POINT('Ctrl Pts',(0.363857027480884,10.0697078423812,258.886209595194));
#15959=CARTESIAN_POINT('Ctrl Pts',(0.250367525613926,10.2392345429506,258.886209595194));
#15960=CARTESIAN_POINT('Ctrl Pts',(0.130333176594055,10.4039506937353,258.886209595194));
#15961=CARTESIAN_POINT('Ctrl Pts',(0.0103337666115684,10.5686188997126,
258.886209595194));
#15962=CARTESIAN_POINT('Ctrl Pts',(-0.116207256219615,10.7284798091608,
258.886209595194));
#15963=CARTESIAN_POINT('Ctrl Pts',(-0.248971466524913,10.8831592822246,
258.886209595194));
#15964=CARTESIAN_POINT('Ctrl Pts',(-0.317445405170305,10.9629361492275,
258.886209595194));
#15965=CARTESIAN_POINT('Ctrl Pts',(-0.387575234292688,11.0413340485417,
258.886209595194));
#15966=CARTESIAN_POINT('Ctrl Pts',(-0.459320022478923,11.1182969478255,
258.886209595194));
#15967=CARTESIAN_POINT('Ctrl Pts',(-0.515939682919651,11.1790346450735,
258.886209595194));
#15968=CARTESIAN_POINT('Ctrl Pts',(-0.573565190357813,11.2388785523942,
258.886209595194));
#15969=CARTESIAN_POINT('Ctrl Pts',(-0.632177086784188,11.2977995896963,
258.886209595194));
#15970=CARTESIAN_POINT('Ctrl Pts',(-0.650664912710916,11.3163849272724,
258.886209595194));
#15971=CARTESIAN_POINT('Ctrl Pts',(-0.669248914573616,11.3348764140862,
258.886209595194));
#15972=CARTESIAN_POINT('Ctrl Pts',(-0.687922396772642,11.3532673475919,
258.886209595194));
#15973=CARTESIAN_POINT('Ctrl Pts',(-0.830665427309727,11.4938505315441,
258.886209595194));
#15974=CARTESIAN_POINT('Ctrl Pts',(-0.978735934932914,11.6286636650011,
258.886209595194));
#15975=CARTESIAN_POINT('Ctrl Pts',(-1.13181485672381,11.7573645070508,258.886209595194));
#15976=CARTESIAN_POINT('Ctrl Pts',(-1.2837913086776,11.885138449468,258.886209595194));
#15977=CARTESIAN_POINT('Ctrl Pts',(-1.44070486494264,12.0068881819309,258.886209595194));
#15978=CARTESIAN_POINT('Ctrl Pts',(-1.60226714821513,12.1222335635334,258.886209595194));
#15979=CARTESIAN_POINT('Ctrl Pts',(-1.76109169330005,12.2356243710263,258.886209595194));
#15980=CARTESIAN_POINT('Ctrl Pts',(-1.92440928861502,12.3428262801963,258.886209595194));
#15981=CARTESIAN_POINT('Ctrl Pts',(-2.09196087277376,12.4434299668365,258.886209595194));
#15982=CARTESIAN_POINT('Ctrl Pts',(-2.120175705855,12.4603711150815,258.886209595194));
#15983=CARTESIAN_POINT('Ctrl Pts',(-2.14851062563325,12.4771250413085,258.886209595194));
#15984=CARTESIAN_POINT('Ctrl Pts',(-2.17696442109716,12.4936896459294,258.886209595194));
#15985=CARTESIAN_POINT('Ctrl Pts',(-5.02255860044619,15.1738049495012,244.886209595194));
#15986=CARTESIAN_POINT('Ctrl Pts',(-6.45069372495988,15.415165992917,244.951210148077));
#15987=CARTESIAN_POINT('Ctrl Pts',(-7.93845566333615,15.2997061708998,245.01621070096));
#15988=CARTESIAN_POINT('Ctrl Pts',(-9.3116386098082,14.84067805856,245.081211253844));
#15989=CARTESIAN_POINT('Ctrl Pts',(-10.6848215562803,14.3816499462201,245.146211806727));
#15990=CARTESIAN_POINT('Ctrl Pts',(-11.9434255108482,13.5790535435577,245.21121235961));
#15991=CARTESIAN_POINT('Ctrl Pts',(-12.9389692831164,12.5275258634565,245.276212912493));
#15992=CARTESIAN_POINT('Ctrl Pts',(-13.9345130553847,11.4759981833554,245.341213465377));
#15993=CARTESIAN_POINT('Ctrl Pts',(-14.6669966453531,10.1755392258155,245.40621401826));
#15994=CARTESIAN_POINT('Ctrl Pts',(-15.0503376992346,8.77919267417778,245.471214571143));
#15995=CARTESIAN_POINT('Ctrl Pts',(-15.259915832765,8.01578969114034,245.506751319461));
#15996=CARTESIAN_POINT('Ctrl Pts',(-15.365136378047,7.22372621266417,245.542288067779));
#15997=CARTESIAN_POINT('Ctrl Pts',(-15.3653307732302,6.43170986456378,245.577824816097));
#15998=CARTESIAN_POINT('Origin',(-6.5,6.43177298256785,244.886209595194));
#15999=CARTESIAN_POINT('',(-17.5,6.43177298256785,244.886209595194));
#16000=CARTESIAN_POINT('Origin',(-6.5,6.43177298256785,244.886209595194));
#16001=CARTESIAN_POINT('Origin',(-6.5,6.43177298256785,244.886209595194));
#16002=CARTESIAN_POINT('Origin',(-6.5,6.43177298256785,260.886209595194));
#16003=CARTESIAN_POINT('',(-17.5,6.43177298256785,236.886209595194));
#16004=CARTESIAN_POINT('Origin',(-6.5,6.43177298256785,236.886209595194));
#16005=CARTESIAN_POINT('',(-17.5,6.43177298256785,260.886209595194));
#16006=CARTESIAN_POINT('Origin',(-6.5,6.43177298256785,236.886209595194));
#16007=CARTESIAN_POINT('',(-13.5,6.43177298256785,236.886209595194));
#16008=CARTESIAN_POINT('Origin',(-6.5,6.43177298256785,236.886209595194));
#16009=CARTESIAN_POINT('Origin',(-6.5,6.43177298256785,258.886209595194));
#16010=CARTESIAN_POINT('',(-13.5,6.43177298256785,258.886209595194));
#16011=CARTESIAN_POINT('Origin',(-6.5,6.43177298256785,258.886209595194));
#16012=CARTESIAN_POINT('Origin',(-6.5,6.43177298256785,260.886209595194));
#16013=CARTESIAN_POINT('',(-13.5,6.43177298256785,260.886209595194));
#16014=CARTESIAN_POINT('Origin',(-6.5,6.43177298256785,260.886209595194));
#17022=UNCERTAINTY_MEASURE_WITH_UNIT(LENGTH_MEASURE(0.01),#17043,
'DISTANCE_ACCURACY_VALUE',
'Maximum model space distance between geometric entities at asserted c
onnectivities');
#17028=UNCERTAINTY_MEASURE_WITH_UNIT(LENGTH_MEASURE(0.01),#17043,
'DISTANCE_ACCURACY_VALUE',
'Maximum model space distance between geometric entities at asserted c
onnectivities');
#17036=(
GEOMETRIC_REPRESENTATION_CONTEXT(3)
GLOBAL_UNCERTAINTY_ASSIGNED_CONTEXT((#17022))
GLOBAL_UNIT_ASSIGNED_CONTEXT((#17043,#17045,#17046))
REPRESENTATION_CONTEXT('','3D')
);
#17042=(
GEOMETRIC_REPRESENTATION_CONTEXT(3)
GLOBAL_UNCERTAINTY_ASSIGNED_CONTEXT((#17028))
GLOBAL_UNIT_ASSIGNED_CONTEXT((#17043,#17045,#17046))
REPRESENTATION_CONTEXT('','3D')
);
#17043=(
LENGTH_UNIT()
NAMED_UNIT(*)
SI_UNIT(.MILLI.,.METRE.)
);
#17045=(
NAMED_UNIT(*)
PLANE_ANGLE_UNIT()
SI_UNIT($,.RADIAN.)
);
#17046=(
NAMED_UNIT(*)
SI_UNIT($,.STERADIAN.)
SOLID_ANGLE_UNIT()
);
#17054=SHAPE_DEFINITION_REPRESENTATION(#17067,#17092);
#17067=PRODUCT_DEFINITION_SHAPE('',$,#17106);
#17092=SHAPE_REPRESENTATION('',(#8908),#17036);
#17098=PRODUCT_DEFINITION_CONTEXT('part definition',#17139,'design');
#17106=PRODUCT_DEFINITION('Nut','Nut',#17119,#17098);
#17119=PRODUCT_DEFINITION_FORMATION('',$,#17148);
#17139=APPLICATION_CONTEXT(
'Core Data for Automotive Mechanical Design Process');
#17140=PRODUCT_CONTEXT('part definition',#17139,'mechanical');
#17148=PRODUCT('Nut','Nut',$,(#17140));
#17154=PRESENTATION_STYLE_ASSIGNMENT((#17155));
#17155=SURFACE_STYLE_USAGE(.BOTH.,#17156);
#17156=SURFACE_SIDE_STYLE('',(#17157));
#17157=SURFACE_STYLE_FILL_AREA(#17158);
#17158=FILL_AREA_STYLE('Steel - Satin',(#17159));
#17159=FILL_AREA_STYLE_COLOUR('Steel - Satin',#17160);
#17160=COLOUR_RGB('Steel - Satin', 0.09019608, 0.27058824, 0.51372549);
ENDSEC;
END-ISO-10303-21;
